ISO-10303-21;
HEADER;
FILE_DESCRIPTION (('STEP AP214'),
    '1' );
FILE_NAME ('Part4.step',
    '2026-11-01T06:29:40',
    ( '' ),
    ( '' ),
    'SwSTEP 2.0',
    'SolidWorks 2024',
    '' );
FILE_SCHEMA (( 'AUTOMOTIVE_DESIGN' ));
ENDSEC;

DATA;
#30=EDGE_LOOP ( 'NONE', ( #17884, #17618, #18763, #13200 ) ) ;
#60=VECTOR ( 'NONE', #12496, 1000.000000000000000 ) ;
#80=DIRECTION ( 'NONE',  ( 0.000000000000000000, -7.137148015447440312E-15, 1.000000000000000000 ) ) ;
#99=LINE ( 'NONE', #6410, #14355 ) ;
#140=VERTEX_POINT ( 'NONE', #7427 ) ;
#143=AXIS2_PLACEMENT_3D ( 'NONE', #8052, #14338, #11231 ) ;
#194=DIRECTION ( 'NONE',  ( -1.000000000000000000, -0.000000000000000000, -0.000000000000000000 ) ) ;
#213=SURFACE_SIDE_STYLE ('',( #11233 ) ) ;
#227=ORIENTED_EDGE ( 'NONE', *, *, #4552, .F. ) ;
#231=CARTESIAN_POINT ( 'NONE',  ( 10.00000000000000000, 381.0487089519837127, -150.0000000000032685 ) ) ;
#251=DIRECTION ( 'NONE',  ( 1.000000000000000000, 0.000000000000000000, 0.000000000000000000 ) ) ;
#261=SURFACE_STYLE_FILL_AREA ( #19230 ) ;
#265=( NAMED_UNIT ( * ) PLANE_ANGLE_UNIT ( ) SI_UNIT ( $, .RADIAN. ) );
#286=LINE ( 'NONE', #7727, #4968 ) ;
#288=EDGE_CURVE ( 'NONE', #8097, #2140, #18654, .T. ) ;
#311=STYLED_ITEM ( 'NONE', ( #8924 ), #10883 ) ;
#332=DIRECTION ( 'NONE',  ( 0.000000000000000000, 0.000000000000000000, -1.000000000000000000 ) ) ;
#363=CIRCLE ( 'NONE', #17149, 3.300000000000011369 ) ;
#374=MECHANICAL_DESIGN_GEOMETRIC_PRESENTATION_REPRESENTATION('',(#10253),#17163);
#416=UNCERTAINTY_MEASURE_WITH_UNIT (LENGTH_MEASURE( 1.000000000000000082E-05 ), #13486, 'distance_accuracy_value', 'NONE');
#426=UNCERTAINTY_MEASURE_WITH_UNIT (LENGTH_MEASURE( 1.000000000000000082E-05 ), #10471, 'distance_accuracy_value', 'NONE');
#427=EDGE_LOOP ( 'NONE', ( #3778, #10463, #12858, #6820 ) ) ;
#431=EDGE_CURVE ( 'NONE', #10962, #10668, #11126, .T. ) ;
#454=COLOUR_RGB ( '', 0.40784314, 0.44705882, 0.49803922) ;
#462=( NAMED_UNIT ( * ) SI_UNIT ( $, .STERADIAN. ) SOLID_ANGLE_UNIT ( ) );
#483=CARTESIAN_POINT ( 'NONE',  ( 10.00000000000000000, 306.0487089519832011, -75.00000000000380851 ) ) ;
#514=DIRECTION ( 'NONE',  ( 1.000000000000000000, -0.000000000000000000, 0.000000000000000000 ) ) ;
#548=VERTEX_POINT ( 'NONE', #13204 ) ;
#568=EDGE_CURVE ( 'NONE', #9832, #5553, #10017, .T. ) ;
#574=EDGE_CURVE ( 'NONE', #2140, #4998, #18228, .T. ) ;
#576=VECTOR ( 'NONE', #1762, 1000.000000000000000 ) ;
#577=CIRCLE ( 'NONE', #20325, 3.300000000000011369 ) ;
#606=CARTESIAN_POINT ( 'NONE',  ( 10.00000000000000000, 309.2289037985885898, -83.18019484660915452 ) ) ;
#637=( LENGTH_UNIT ( ) NAMED_UNIT ( * ) SI_UNIT ( .MILLI., .METRE. ) );
#695=FILL_AREA_STYLE ('',( #7211 ) ) ;
#712=ORIENTED_EDGE ( 'NONE', *, *, #19124, .F. ) ;
#762=EDGE_LOOP ( 'NONE', ( #10042, #10538 ) ) ;
#764=AXIS2_PLACEMENT_3D ( 'NONE', #7394, #5745, #11928 ) ;
#789=CARTESIAN_POINT ( 'NONE',  ( 10.00000000000000000, 372.8685141053778693, -86.48019484660871115 ) ) ;
#801=PRESENTATION_STYLE_ASSIGNMENT (( #19643 ) ) ;
#841=COLOUR_RGB ( '', 0.72549020, 0.75294118, 0.79215686) ;
#854=UNCERTAINTY_MEASURE_WITH_UNIT (LENGTH_MEASURE( 1.000000000000000082E-05 ), #13674, 'distance_accuracy_value', 'NONE');
#867=VERTEX_POINT ( 'NONE', #483 ) ;
#872=ORIENTED_EDGE ( 'NONE', *, *, #10810, .F. ) ;
#892=CARTESIAN_POINT ( 'NONE',  ( 0.000000000000000000, 309.2289037985890445, -146.8198051533984199 ) ) ;
#917=LINE ( 'NONE', #7452, #14906 ) ;
#927=FACE_BOUND ( 'NONE', #7352, .T. ) ;
#930=ADVANCED_FACE ( 'NONE', ( #16471 ), #2319, .F. ) ;
#967=DIRECTION ( 'NONE',  ( 0.000000000000000000, 1.000000000000000000, -0.000000000000000000 ) ) ;
#970=SURFACE_SIDE_STYLE ('',( #15127 ) ) ;
#997=EDGE_LOOP ( 'NONE', ( #19667, #16150 ) ) ;
#1015=DIRECTION ( 'NONE',  ( 0.000000000000000000, 7.137148015447440312E-15, -1.000000000000000000 ) ) ;
#1020=EDGE_CURVE ( 'NONE', #13941, #9832, #16681, .T. ) ;
#1059=SURFACE_STYLE_FILL_AREA ( #13567 ) ;
#1081=ORIENTED_EDGE ( 'NONE', *, *, #13213, .T. ) ;
#1088=MECHANICAL_DESIGN_GEOMETRIC_PRESENTATION_REPRESENTATION('',(#4747),#9015);
#1107=ORIENTED_EDGE ( 'NONE', *, *, #2833, .F. ) ;
#1112=CARTESIAN_POINT ( 'NONE',  ( 10.00000000000000000, 372.8685141053783241, -143.5198051533979537 ) ) ;
#1185=( NAMED_UNIT ( * ) PLANE_ANGLE_UNIT ( ) SI_UNIT ( $, .RADIAN. ) );
#1210=CARTESIAN_POINT ( 'NONE',  ( 0.000000000000000000, 309.2289037985890445, -150.1198051533984597 ) ) ;
#1211=FILL_AREA_STYLE ('',( #15377 ) ) ;
#1219=VECTOR ( 'NONE', #13981, 1000.000000000000000 ) ;
#1270=( GEOMETRIC_REPRESENTATION_CONTEXT ( 3 ) GLOBAL_UNCERTAINTY_ASSIGNED_CONTEXT ( ( #8267 ) ) GLOBAL_UNIT_ASSIGNED_CONTEXT ( ( #7302, #19842, #18311 ) ) REPRESENTATION_CONTEXT ( 'NONE', 'WORKASPACE' ) );
#1281=SURFACE_STYLE_USAGE ( .BOTH. , #1392 ) ;
#1284=CARTESIAN_POINT ( 'NONE',  ( 10.00000000000000000, 309.2289037985890445, -146.8198051533984199 ) ) ;
#1286=( NAMED_UNIT ( * ) SI_UNIT ( $, .STERADIAN. ) SOLID_ANGLE_UNIT ( ) );
#1299=ORIENTED_EDGE ( 'NONE', *, *, #17199, .F. ) ;
#1306=( NAMED_UNIT ( * ) PLANE_ANGLE_UNIT ( ) SI_UNIT ( $, .RADIAN. ) );
#1370=CIRCLE ( 'NONE', #12951, 5.000000000000004441 ) ;
#1371=FILL_AREA_STYLE ('',( #7807 ) ) ;
#1380=PRODUCT_DEFINITION ( 'UNKNOWN', '', #5359, #8846 ) ;
#1386=CARTESIAN_POINT ( 'NONE',  ( 10.00000000000000000, 372.8685141053783241, -143.5198051533979537 ) ) ;
#1392=SURFACE_SIDE_STYLE ('',( #9156 ) ) ;
#1415=STYLED_ITEM ( 'NONE', ( #10441 ), #19301 ) ;
#1421=DIRECTION ( 'NONE',  ( 1.000000000000000000, -0.000000000000000000, 0.000000000000000000 ) ) ;
#1500=ORIENTED_EDGE ( 'NONE', *, *, #3595, .F. ) ;
#1501=MECHANICAL_DESIGN_GEOMETRIC_PRESENTATION_REPRESENTATION('',(#14036),#16371);
#1531=( NAMED_UNIT ( * ) PLANE_ANGLE_UNIT ( ) SI_UNIT ( $, .RADIAN. ) );
#1538=COLOUR_RGB ( '', 0.40784314, 0.44705882, 0.49803922) ;
#1551=DIRECTION ( 'NONE',  ( -1.000000000000000000, -0.000000000000000000, -0.000000000000000000 ) ) ;
#1556=CARTESIAN_POINT ( 'NONE',  ( 0.000000000000000000, 372.8685141053783241, -150.1198051533980049 ) ) ;
#1568=ORIENTED_EDGE ( 'NONE', *, *, #4226, .T. ) ;
#1569=DIRECTION ( 'NONE',  ( 1.000000000000000000, -0.000000000000000000, 0.000000000000000000 ) ) ;
#1583=MANIFOLD_SOLID_BREP ( 'Boss-Extrude2', #14588 ) ;
#1596=( GEOMETRIC_REPRESENTATION_CONTEXT ( 3 ) GLOBAL_UNCERTAINTY_ASSIGNED_CONTEXT ( ( #15000 ) ) GLOBAL_UNIT_ASSIGNED_CONTEXT ( ( #16980, #6047, #15331 ) ) REPRESENTATION_CONTEXT ( 'NONE', 'WORKASPACE' ) );
#1622=MECHANICAL_DESIGN_GEOMETRIC_PRESENTATION_REPRESENTATION('',(#11542),#14185);
#1633=CIRCLE ( 'NONE', #14507, 18.49999999999998934 ) ;
#1655=EDGE_CURVE ( 'NONE', #11104, #4860, #20076, .T. ) ;
#1663=VERTEX_POINT ( 'NONE', #15579 ) ;
#1670=FILL_AREA_STYLE ('',( #16055 ) ) ;
#1690=DIRECTION ( 'NONE',  ( 0.000000000000000000, 0.000000000000000000, 1.000000000000000000 ) ) ;
#1707=( NAMED_UNIT ( * ) SI_UNIT ( $, .STERADIAN. ) SOLID_ANGLE_UNIT ( ) );
#1709=ADVANCED_FACE ( 'NONE', ( #17311 ), #9473, .T. ) ;
#1724=EDGE_LOOP ( 'NONE', ( #712, #3861 ) ) ;
#1726=SURFACE_SIDE_STYLE ('',( #3291 ) ) ;
#1730=CARTESIAN_POINT ( 'NONE',  ( 10.00000000000000000, 309.2289037985890445, -143.5198051533984085 ) ) ;
#1735=DIRECTION ( 'NONE',  ( 0.000000000000000000, 0.000000000000000000, -1.000000000000000000 ) ) ;
#1741=FILL_AREA_STYLE_COLOUR ( '', #7350 ) ;
#1762=DIRECTION ( 'NONE',  ( 0.000000000000000000, 7.137148015447440312E-15, -1.000000000000000000 ) ) ;
#1781=COLOUR_RGB ( '', 0.40784314, 0.44705882, 0.49803922) ;
#1783=COLOUR_RGB ( '', 0.08235294, 0.09019608, 0.10196078) ;
#1792=LINE ( 'NONE', #18996, #5300 ) ;
#1827=CARTESIAN_POINT ( 'NONE',  ( 10.00000000000000000, 309.2289037985890445, -150.1198051533984597 ) ) ;
#1843=( GEOMETRIC_REPRESENTATION_CONTEXT ( 3 ) GLOBAL_UNCERTAINTY_ASSIGNED_CONTEXT ( ( #17619 ) ) GLOBAL_UNIT_ASSIGNED_CONTEXT ( ( #3816, #2551, #19747 ) ) REPRESENTATION_CONTEXT ( 'NONE', 'WORKASPACE' ) );
#1861=ORIENTED_EDGE ( 'NONE', *, *, #8741, .F. ) ;
#1870=FILL_AREA_STYLE ('',( #11159 ) ) ;
#1882=FACE_OUTER_BOUND ( 'NONE', #14799, .T. ) ;
#1899=VECTOR ( 'NONE', #17682, 1000.000000000000000 ) ;
#1901=EDGE_CURVE ( 'NONE', #6758, #17942, #11703, .T. ) ;
#1930=CARTESIAN_POINT ( 'NONE',  ( 0.000000000000000000, 341.0487089519837696, -133.5000000000032969 ) ) ;
#1935=EDGE_CURVE ( 'NONE', #867, #548, #4785, .T. ) ;
#1949=VERTEX_POINT ( 'NONE', #2572 ) ;
#1965=DIRECTION ( 'NONE',  ( -0.000000000000000000, -1.000000000000000000, -0.000000000000000000 ) ) ;
#1993=DIRECTION ( 'NONE',  ( 1.000000000000000000, -0.000000000000000000, 0.000000000000000000 ) ) ;
#2030=AXIS2_PLACEMENT_3D ( 'NONE', #10574, #10675, #16978 ) ;
#2036=VECTOR ( 'NONE', #9134, 1000.000000000000000 ) ;
#2058=UNCERTAINTY_MEASURE_WITH_UNIT (LENGTH_MEASURE( 1.000000000000000082E-05 ), #8285, 'distance_accuracy_value', 'NONE');
#2127=STYLED_ITEM ( 'NONE', ( #9038 ), #15379 ) ;
#2140=VERTEX_POINT ( 'NONE', #7472 ) ;
#2201=ORIENTED_EDGE ( 'NONE', *, *, #6920, .F. ) ;
#2203=FILL_AREA_STYLE_COLOUR ( '', #14563 ) ;
#2211=AXIS2_PLACEMENT_3D ( 'NONE', #3801, #17899, #10271 ) ;
#2233=ORIENTED_EDGE ( 'NONE', *, *, #16026, .T. ) ;
#2246=EDGE_CURVE ( 'NONE', #4537, #867, #11363, .T. ) ;
#2260=VERTEX_POINT ( 'NONE', #17745 ) ;
#2319=CYLINDRICAL_SURFACE ( 'NONE', #19561, 18.49999999999998934 ) ;
#2327=DIRECTION ( 'NONE',  ( 0.000000000000000000, 0.000000000000000000, -1.000000000000000000 ) ) ;
#2330=FILL_AREA_STYLE ('',( #18400 ) ) ;
#2406=FILL_AREA_STYLE_COLOUR ( '', #8038 ) ;
#2457=AXIS2_PLACEMENT_3D ( 'NONE', #18199, #967, #7298 ) ;
#2545=ADVANCED_FACE ( 'NONE', ( #4546 ), #8970, .T. ) ;
#2551=( NAMED_UNIT ( * ) PLANE_ANGLE_UNIT ( ) SI_UNIT ( $, .RADIAN. ) );
#2555=PRESENTATION_STYLE_ASSIGNMENT (( #1281 ) ) ;
#2572=CARTESIAN_POINT ( 'NONE',  ( 0.000000000000000000, 368.2663108437010919, -142.2176018917206761 ) ) ;
#2635=FILL_AREA_STYLE_COLOUR ( '', #10508 ) ;
#2643=DIRECTION ( 'NONE',  ( 0.000000000000000000, 7.137148015447440312E-15, -1.000000000000000000 ) ) ;
#2673=DIRECTION ( 'NONE',  ( 0.000000000000000000, 0.000000000000000000, -1.000000000000000000 ) ) ;
#2690=EDGE_CURVE ( 'NONE', #4515, #8097, #13699, .T. ) ;
#2695=EDGE_CURVE ( 'NONE', #3271, #8713, #99, .T. ) ;
#2708=STYLED_ITEM ( 'NONE', ( #18301 ), #3313 ) ;
#2741=AXIS2_PLACEMENT_3D ( 'NONE', #5042, #3500, #8234 ) ;
#2742=CARTESIAN_POINT ( 'NONE',  ( 10.00000000000000000, 301.0487089519832011, -80.00000000000387956 ) ) ;
#2760=CARTESIAN_POINT ( 'NONE',  ( -75.00000000000000000, 368.2663108437010919, -142.2176018917206761 ) ) ;
#2768=COLOUR_RGB ( '', 0.31764706, 0.68627451, 0.89019608) ;
#2784=( GEOMETRIC_REPRESENTATION_CONTEXT ( 3 ) GLOBAL_UNCERTAINTY_ASSIGNED_CONTEXT ( ( #854 ) ) GLOBAL_UNIT_ASSIGNED_CONTEXT ( ( #13674, #16868, #4289 ) ) REPRESENTATION_CONTEXT ( 'NONE', 'WORKASPACE' ) );
#2833=EDGE_CURVE ( 'NONE', #10340, #1663, #13714, .T. ) ;
#2856=SURFACE_STYLE_USAGE ( .BOTH. , #11178 ) ;
#2860=FILL_AREA_STYLE ('',( #10707 ) ) ;
#2863=CYLINDRICAL_SURFACE ( 'NONE', #16746, 3.300000000000025135 ) ;
#2870=CYLINDRICAL_SURFACE ( 'NONE', #18389, 4.999999999999990230 ) ;
#2916=ORIENTED_EDGE ( 'NONE', *, *, #1935, .T. ) ;
#2934=CARTESIAN_POINT ( 'NONE',  ( 10.00000000000000000, 376.0487089519837127, -150.0000000000033538 ) ) ;
#2949=ADVANCED_FACE ( 'NONE', ( #20057 ), #12242, .F. ) ;
#2963=DIRECTION ( 'NONE',  ( 0.000000000000000000, 0.000000000000000000, 1.000000000000000000 ) ) ;
#3015=SURFACE_SIDE_STYLE ('',( #9510 ) ) ;
#3038=DIRECTION ( 'NONE',  ( 0.000000000000000000, 0.000000000000000000, -1.000000000000000000 ) ) ;
#3046=( NAMED_UNIT ( * ) SI_UNIT ( $, .STERADIAN. ) SOLID_ANGLE_UNIT ( ) );
#3048=ORIENTED_EDGE ( 'NONE', *, *, #4890, .T. ) ;
#3056=ORIENTED_EDGE ( 'NONE', *, *, #13892, .F. ) ;
#3076=LINE ( 'NONE', #6594, #4315 ) ;
#3082=ORIENTED_EDGE ( 'NONE', *, *, #7846, .F. ) ;
#3121=MECHANICAL_DESIGN_GEOMETRIC_PRESENTATION_REPRESENTATION('',(#14320),#10681);
#3132=LINE ( 'NONE', #15724, #15078 ) ;
#3183=CARTESIAN_POINT ( 'NONE',  ( 0.000000000000000000, 309.2289037985885898, -83.18019484660915452 ) ) ;
#3189=CARTESIAN_POINT ( 'NONE',  ( 0.000000000000000000, 301.0487089519837127, -150.0000000000038369 ) ) ;
#3231=DIRECTION ( 'NONE',  ( 0.000000000000000000, 0.000000000000000000, -1.000000000000000000 ) ) ;
#3271=VERTEX_POINT ( 'NONE', #6045 ) ;
#3277=CARTESIAN_POINT ( 'NONE',  ( 0.000000000000000000, 306.0487089519832011, -75.00000000000380851 ) ) ;
#3282=CARTESIAN_POINT ( 'NONE',  ( 10.00000000000000000, 301.0487089519826327, 2.148629195649657075E-12 ) ) ;
#3291=SURFACE_STYLE_FILL_AREA ( #15882 ) ;
#3313=ADVANCED_FACE ( 'NONE', ( #12213 ), #12120, .T. ) ;
#3318=ORIENTED_EDGE ( 'NONE', *, *, #4145, .F. ) ;
#3322=CIRCLE ( 'NONE', #9248, 3.300000000000011369 ) ;
#3330=CARTESIAN_POINT ( 'NONE',  ( 10.00000000000000000, 372.8685141053783241, -146.8198051533979935 ) ) ;
#3375=ORIENTED_EDGE ( 'NONE', *, *, #7006, .T. ) ;
#3381=LINE ( 'NONE', #6803, #17772 ) ;
#3382=CARTESIAN_POINT ( 'NONE',  ( 10.00000000000000000, 372.8685141053778693, -83.18019484660869978 ) ) ;
#3414=PRESENTATION_STYLE_ASSIGNMENT (( #6512 ) ) ;
#3442=CARTESIAN_POINT ( 'NONE',  ( 10.00000000000000000, 309.2289037985885898, -86.48019484660916589 ) ) ;
#3457=( GEOMETRIC_REPRESENTATION_CONTEXT ( 3 ) GLOBAL_UNCERTAINTY_ASSIGNED_CONTEXT ( ( #416 ) ) GLOBAL_UNIT_ASSIGNED_CONTEXT ( ( #13486, #11931, #8839 ) ) REPRESENTATION_CONTEXT ( 'NONE', 'WORKASPACE' ) );
#3475=CARTESIAN_POINT ( 'NONE',  ( 0.000000000000000000, 301.0487089519832011, -80.00000000000387956 ) ) ;
#3500=DIRECTION ( 'NONE',  ( 0.000000000000000000, 0.000000000000000000, 1.000000000000000000 ) ) ;
#3577=EDGE_CURVE ( 'NONE', #13735, #16276, #6207, .T. ) ;
#3595=EDGE_CURVE ( 'NONE', #16084, #4680, #1370, .T. ) ;
#3631=STYLED_ITEM ( 'NONE', ( #18404 ), #16376 ) ;
#3656=ORIENTED_EDGE ( 'NONE', *, *, #18201, .T. ) ;
#3673=CARTESIAN_POINT ( 'NONE',  ( 0.000000000000000000, 341.0487089519837696, -96.50000000000331113 ) ) ;
#3679=CARTESIAN_POINT ( 'NONE',  ( 0.000000000000000000, 309.2289037985885898, -83.18019484660915452 ) ) ;
#3686=DIRECTION ( 'NONE',  ( 0.000000000000000000, 0.000000000000000000, 1.000000000000000000 ) ) ;
#3687=VECTOR ( 'NONE', #10155, 1000.000000000000000 ) ;
#3690=SURFACE_STYLE_USAGE ( .BOTH. , #13098 ) ;
#3711=AXIS2_PLACEMENT_3D ( 'NONE', #3382, #18820, #17389 ) ;
#3720=STYLED_ITEM ( 'NONE', ( #5016 ), #18322 ) ;
#3756=VECTOR ( 'NONE', #7577, 1000.000000000000000 ) ;
#3778=ORIENTED_EDGE ( 'NONE', *, *, #4971, .F. ) ;
#3785=MECHANICAL_DESIGN_GEOMETRIC_PRESENTATION_REPRESENTATION('',(#12323),#2784);
#3801=CARTESIAN_POINT ( 'NONE',  ( 10.00000000000000000, 309.2289037985885898, -83.18019484660915452 ) ) ;
#3816=( LENGTH_UNIT ( ) NAMED_UNIT ( * ) SI_UNIT ( .MILLI., .METRE. ) );
#3830=( GEOMETRIC_REPRESENTATION_CONTEXT ( 3 ) GLOBAL_UNCERTAINTY_ASSIGNED_CONTEXT ( ( #11360 ) ) GLOBAL_UNIT_ASSIGNED_CONTEXT ( ( #17025, #1306, #20194 ) ) REPRESENTATION_CONTEXT ( 'NONE', 'WORKASPACE' ) );
#3848=LINE ( 'NONE', #11780, #9075 ) ;
#3855=CARTESIAN_POINT ( 'NONE',  ( 10.00000000000000000, 309.2289037985890445, -146.8198051533984199 ) ) ;
#3861=ORIENTED_EDGE ( 'NONE', *, *, #16026, .F. ) ;
#3944=SURFACE_SIDE_STYLE ('',( #14868 ) ) ;
#4004=ADVANCED_FACE ( 'NONE', ( #17008 ), #2863, .F. ) ;
#4025=( GEOMETRIC_REPRESENTATION_CONTEXT ( 3 ) GLOBAL_UNCERTAINTY_ASSIGNED_CONTEXT ( ( #426 ) ) GLOBAL_UNIT_ASSIGNED_CONTEXT ( ( #10471, #13865, #13678 ) ) REPRESENTATION_CONTEXT ( 'NONE', 'WORKASPACE' ) );
#4067=CIRCLE ( 'NONE', #19844, 5.000000000000004441 ) ;
#4074=FILL_AREA_STYLE ('',( #20008 ) ) ;
#4085=CIRCLE ( 'NONE', #5728, 18.49999999999998934 ) ;
#4101=STYLED_ITEM ( 'NONE', ( #5826 ), #12671 ) ;
#4103=PLANE ( 'NONE',  #11628 ) ;
#4115=UNCERTAINTY_MEASURE_WITH_UNIT (LENGTH_MEASURE( 1.000000000000000082E-05 ), #17577, 'distance_accuracy_value', 'NONE');
#4117=EDGE_CURVE ( 'NONE', #5163, #140, #577, .T. ) ;
#4141=CARTESIAN_POINT ( 'NONE',  ( 10.00000000000000000, 341.0487089519837696, -115.0000000000032969 ) ) ;
#4145=EDGE_CURVE ( 'NONE', #10045, #12099, #9662, .T. ) ;
#4168=LINE ( 'NONE', #10333, #10332 ) ;
#4179=STYLED_ITEM ( 'NONE', ( #801 ), #9578 ) ;
#4192=VERTEX_POINT ( 'NONE', #19135 ) ;
#4209=DIRECTION ( 'NONE',  ( 0.000000000000000000, -1.000000000000000000, -7.137148015447440312E-15 ) ) ;
#4212=SURFACE_STYLE_USAGE ( .BOTH. , #970 ) ;
#4214=AXIS2_PLACEMENT_3D ( 'NONE', #10170, #16477, #2327 ) ;
#4226=EDGE_CURVE ( 'NONE', #1663, #10340, #10466, .T. ) ;
#4235=DIRECTION ( 'NONE',  ( 0.000000000000000000, 0.000000000000000000, -1.000000000000000000 ) ) ;
#4256=SURFACE_STYLE_FILL_AREA ( #5809 ) ;
#4272=SURFACE_SIDE_STYLE ('',( #7177 ) ) ;
#4289=( NAMED_UNIT ( * ) SI_UNIT ( $, .STERADIAN. ) SOLID_ANGLE_UNIT ( ) );
#4315=VECTOR ( 'NONE', #194, 1000.000000000000000 ) ;
#4348=EDGE_CURVE ( 'NONE', #6703, #4581, #7507, .T. ) ;
#4378=ORIENTED_EDGE ( 'NONE', *, *, #1935, .F. ) ;
#4388=DIRECTION ( 'NONE',  ( 0.000000000000000000, 0.000000000000000000, 1.000000000000000000 ) ) ;
#4394=DIRECTION ( 'NONE',  ( -1.000000000000000000, -0.000000000000000000, -0.000000000000000000 ) ) ;
#4411=CARTESIAN_POINT ( 'NONE',  ( 0.000000000000000000, 372.8685141053778693, -83.18019484660869978 ) ) ;
#4412=DIRECTION ( 'NONE',  ( -1.000000000000000000, -0.000000000000000000, -0.000000000000000000 ) ) ;
#4445=PRESENTATION_STYLE_ASSIGNMENT (( #7744 ) ) ;
#4452=DIRECTION ( 'NONE',  ( 0.000000000000000000, -1.000000000000000000, -7.137148015447440312E-15 ) ) ;
#4457=FACE_OUTER_BOUND ( 'NONE', #9214, .T. ) ;
#4515=VERTEX_POINT ( 'NONE', #7395 ) ;
#4537=VERTEX_POINT ( 'NONE', #7587 ) ;
#4546=FACE_OUTER_BOUND ( 'NONE', #7410, .T. ) ;
#4548=DIRECTION ( 'NONE',  ( 0.000000000000000000, -7.137148015447440312E-15, 1.000000000000000000 ) ) ;
#4552=EDGE_CURVE ( 'NONE', #548, #4581, #16877, .T. ) ;
#4581=VERTEX_POINT ( 'NONE', #3475 ) ;
#4598=FILL_AREA_STYLE ('',( #2635 ) ) ;
#4611=EDGE_CURVE ( 'NONE', #7675, #19389, #15092, .T. ) ;
#4653=DIRECTION ( 'NONE',  ( 0.000000000000000000, 7.137148015447440312E-15, -1.000000000000000000 ) ) ;
#4672=DIRECTION ( 'NONE',  ( -1.000000000000000000, -0.000000000000000000, -0.000000000000000000 ) ) ;
#4680=VERTEX_POINT ( 'NONE', #5519 ) ;
#4686=DIRECTION ( 'NONE',  ( 0.000000000000000000, -1.000000000000000000, 0.000000000000000000 ) ) ;
#4688=EDGE_CURVE ( 'NONE', #17942, #7810, #18067, .T. ) ;
#4691=MECHANICAL_DESIGN_GEOMETRIC_PRESENTATION_REPRESENTATION('',(#3720),#8968);
#4699=CARTESIAN_POINT ( 'NONE',  ( 0.000000000000000000, 372.8685141053783241, -146.8198051533979935 ) ) ;
#4706=DIRECTION ( 'NONE',  ( 0.000000000000000000, 0.000000000000000000, -1.000000000000000000 ) ) ;
#4731=SURFACE_SIDE_STYLE ('',( #15460 ) ) ;
#4747=STYLED_ITEM ( 'NONE', ( #12877 ), #12371 ) ;
#4759=AXIS2_PLACEMENT_3D ( 'NONE', #5866, #7514, #10702 ) ;
#4785=CIRCLE ( 'NONE', #14985, 4.999999999999990230 ) ;
#4835=MECHANICAL_DESIGN_GEOMETRIC_PRESENTATION_REPRESENTATION('',(#4179),#1843);
#4860=VERTEX_POINT ( 'NONE', #5828 ) ;
#4876=CARTESIAN_POINT ( 'NONE',  ( 10.00000000000000000, 5.352861011586007481E-13, -75.00000000000599698 ) ) ;
#4890=EDGE_CURVE ( 'NONE', #10259, #13735, #14760, .T. ) ;
#4924=ADVANCED_FACE ( 'NONE', ( #18879 ), #19081, .F. ) ;
#4932=SURFACE_STYLE_FILL_AREA ( #13281 ) ;
#4934=( LENGTH_UNIT ( ) NAMED_UNIT ( * ) SI_UNIT ( .MILLI., .METRE. ) );
#4940=MECHANICAL_DESIGN_GEOMETRIC_PRESENTATION_REPRESENTATION('',(#3631),#1270);
#4945=CARTESIAN_POINT ( 'NONE',  ( 0.000000000000000000, 0.000000000000000000, 0.000000000000000000 ) ) ;
#4952=AXIS2_PLACEMENT_3D ( 'NONE', #3282, #15875, #4979 ) ;
#4968=VECTOR ( 'NONE', #12565, 1000.000000000000000 ) ;
#4971=EDGE_CURVE ( 'NONE', #10340, #5163, #15816, .T. ) ;
#4979=DIRECTION ( 'NONE',  ( 0.000000000000000000, -7.137148015447440312E-15, 1.000000000000000000 ) ) ;
#4998=VERTEX_POINT ( 'NONE', #1556 ) ;
#5016=PRESENTATION_STYLE_ASSIGNMENT (( #14785 ) ) ;
#5025=MECHANICAL_DESIGN_GEOMETRIC_PRESENTATION_REPRESENTATION('',(#2708),#4025);
#5033=ORIENTED_EDGE ( 'NONE', *, *, #13892, .T. ) ;
#5042=CARTESIAN_POINT ( 'NONE',  ( 0.000000000000000000, 0.000000000000000000, 0.000000000000000000 ) ) ;
#5048=( GEOMETRIC_REPRESENTATION_CONTEXT ( 3 ) GLOBAL_UNCERTAINTY_ASSIGNED_CONTEXT ( ( #13810 ) ) GLOBAL_UNIT_ASSIGNED_CONTEXT ( ( #8162, #18307, #16691 ) ) REPRESENTATION_CONTEXT ( 'NONE', 'WORKASPACE' ) );
#5076=EDGE_CURVE ( 'NONE', #1949, #4860, #6645, .T. ) ;
#5084=MECHANICAL_DESIGN_GEOMETRIC_PRESENTATION_REPRESENTATION('',(#14626),#7060);
#5115=( NAMED_UNIT ( * ) SI_UNIT ( $, .STERADIAN. ) SOLID_ANGLE_UNIT ( ) );
#5131=( GEOMETRIC_REPRESENTATION_CONTEXT ( 3 ) GLOBAL_UNCERTAINTY_ASSIGNED_CONTEXT ( ( #8472 ) ) GLOBAL_UNIT_ASSIGNED_CONTEXT ( ( #10032, #7158, #18141 ) ) REPRESENTATION_CONTEXT ( 'NONE', 'WORKASPACE' ) );
#5133=( NAMED_UNIT ( * ) PLANE_ANGLE_UNIT ( ) SI_UNIT ( $, .RADIAN. ) );
#5146=CARTESIAN_POINT ( 'NONE',  ( 10.00000000000000000, 376.0487089519837127, -155.0000000000033253 ) ) ;
#5158=LINE ( 'NONE', #6811, #8404 ) ;
#5163=VERTEX_POINT ( 'NONE', #13732 ) ;
#5167=ORIENTED_EDGE ( 'NONE', *, *, #2246, .T. ) ;
#5171=CARTESIAN_POINT ( 'NONE',  ( 10.00000000000000000, 372.8685141053783241, -146.8198051533979935 ) ) ;
#5193=ORIENTED_EDGE ( 'NONE', *, *, #7913, .T. ) ;
#5199=SURFACE_STYLE_FILL_AREA ( #17245 ) ;
#5204=CARTESIAN_POINT ( 'NONE',  ( 0.000000000000000000, 372.8685141053778693, -83.18019484660869978 ) ) ;
#5235=CARTESIAN_POINT ( 'NONE',  ( 0.000000000000000000, 372.8685141053778693, -79.88019484660868841 ) ) ;
#5262=DIRECTION ( 'NONE',  ( 1.000000000000000000, -0.000000000000000000, 0.000000000000000000 ) ) ;
#5280=MECHANICAL_DESIGN_GEOMETRIC_PRESENTATION_REPRESENTATION('',(#11540),#7906);
#5300=VECTOR ( 'NONE', #15950, 1000.000000000000000 ) ;
#5331=CARTESIAN_POINT ( 'NONE',  ( -75.00000000000000000, 368.2663108437010919, -142.2176018917206761 ) ) ;
#5338=DIRECTION ( 'NONE',  ( 1.000000000000000000, -0.000000000000000000, -0.000000000000000000 ) ) ;
#5359=PRODUCT_DEFINITION_FORMATION_WITH_SPECIFIED_SOURCE ( 'ANY', '', #18958, .NOT_KNOWN. ) ;
#5429=AXIS2_PLACEMENT_3D ( 'NONE', #16758, #19700, #14781 ) ;
#5432=COLOUR_RGB ( '', 0.31764706, 0.68627451, 0.89019608) ;
#5476=EDGE_CURVE ( 'NONE', #4581, #16084, #19840, .T. ) ;
#5480=ORIENTED_EDGE ( 'NONE', *, *, #7913, .F. ) ;
#5497=SURFACE_STYLE_USAGE ( .BOTH. , #5688 ) ;
#5499=ORIENTED_EDGE ( 'NONE', *, *, #18201, .F. ) ;
#5517=STYLED_ITEM ( 'NONE', ( #9254 ), #4004 ) ;
#5519=CARTESIAN_POINT ( 'NONE',  ( 0.000000000000000000, 306.0487089519837696, -155.0000000000038369 ) ) ;
#5546=FACE_OUTER_BOUND ( 'NONE', #18949, .T. ) ;
#5553=VERTEX_POINT ( 'NONE', #12003 ) ;
#5570=ORIENTED_EDGE ( 'NONE', *, *, #5476, .F. ) ;
#5588=DIRECTION ( 'NONE',  ( 0.000000000000000000, 0.000000000000000000, 1.000000000000000000 ) ) ;
#5609=AXIS2_PLACEMENT_3D ( 'NONE', #17267, #20342, #18793 ) ;
#5613=SURFACE_STYLE_USAGE ( .BOTH. , #4272 ) ;
#5616=( LENGTH_UNIT ( ) NAMED_UNIT ( * ) SI_UNIT ( .MILLI., .METRE. ) );
#5620=ORIENTED_EDGE ( 'NONE', *, *, #2690, .T. ) ;
#5657=CARTESIAN_POINT ( 'NONE',  ( 0.000000000000000000, 341.0487089519837696, -96.50000000000331113 ) ) ;
#5665=SURFACE_STYLE_FILL_AREA ( #13897 ) ;
#5688=SURFACE_SIDE_STYLE ('',( #10220 ) ) ;
#5697=CIRCLE ( 'NONE', #17212, 5.000000000000004441 ) ;
#5728=AXIS2_PLACEMENT_3D ( 'NONE', #17961, #6761, #10037 ) ;
#5735=CARTESIAN_POINT ( 'NONE',  ( 0.000000000000000000, 313.8311070602663904, -87.78239810828596035 ) ) ;
#5736=ORIENTED_EDGE ( 'NONE', *, *, #12574, .F. ) ;
#5742=CARTESIAN_POINT ( 'NONE',  ( 10.00000000000000000, 301.0487089519837127, -150.0000000000038369 ) ) ;
#5745=DIRECTION ( 'NONE',  ( -1.000000000000000000, -0.000000000000000000, -0.000000000000000000 ) ) ;
#5763=ORIENTED_EDGE ( 'NONE', *, *, #15301, .F. ) ;
#5768=VECTOR ( 'NONE', #13371, 1000.000000000000000 ) ;
#5784=( LENGTH_UNIT ( ) NAMED_UNIT ( * ) SI_UNIT ( .MILLI., .METRE. ) );
#5798=CARTESIAN_POINT ( 'NONE',  ( 10.00000000000000000, 376.0487089519832011, -80.00000000000332534 ) ) ;
#5809=FILL_AREA_STYLE ('',( #13445 ) ) ;
#5813=COLOUR_RGB ( '', 0.08235294, 0.09019608, 0.10196078) ;
#5818=UNCERTAINTY_MEASURE_WITH_UNIT (LENGTH_MEASURE( 1.000000000000000082E-05 ), #7450, 'distance_accuracy_value', 'NONE');
#5826=PRESENTATION_STYLE_ASSIGNMENT (( #5613 ) ) ;
#5828=CARTESIAN_POINT ( 'NONE',  ( 0.000000000000000000, 313.8311070602663904, -142.2176018917206761 ) ) ;
#5866=CARTESIAN_POINT ( 'NONE',  ( 0.000000000000000000, 372.8685141053783241, -146.8198051533979935 ) ) ;
#5868=LINE ( 'NONE', #2760, #10334 ) ;
#5875=FILL_AREA_STYLE ('',( #6187 ) ) ;
#5881=SURFACE_SIDE_STYLE ('',( #5665 ) ) ;
#5891=SURFACE_SIDE_STYLE ('',( #15162 ) ) ;
#5892=DIRECTION ( 'NONE',  ( -1.000000000000000000, -0.000000000000000000, -0.000000000000000000 ) ) ;
#5894=CARTESIAN_POINT ( 'NONE',  ( 0.000000000000000000, 306.0487089519837127, -150.0000000000038369 ) ) ;
#5903=PLANE ( 'NONE',  #10027 ) ;
#5916=EDGE_LOOP ( 'NONE', ( #1568, #6955, #15573, #7260 ) ) ;
#5935=SURFACE_STYLE_USAGE ( .BOTH. , #12326 ) ;
#5938=FACE_OUTER_BOUND ( 'NONE', #7701, .T. ) ;
#5946=DIRECTION ( 'NONE',  ( 0.000000000000000000, 0.000000000000000000, 1.000000000000000000 ) ) ;
#6045=CARTESIAN_POINT ( 'NONE',  ( -75.00000000000000000, 368.2663108437010919, -87.78239810828596035 ) ) ;
#6047=( NAMED_UNIT ( * ) PLANE_ANGLE_UNIT ( ) SI_UNIT ( $, .RADIAN. ) );
#6057=COLOUR_RGB ( '', 0.09019608, 0.27058824, 0.51372549) ;
#6070=DIRECTION ( 'NONE',  ( 0.000000000000000000, 0.000000000000000000, -1.000000000000000000 ) ) ;
#6083=DIRECTION ( 'NONE',  ( 0.000000000000000000, 0.000000000000000000, -1.000000000000000000 ) ) ;
#6090=( GEOMETRIC_REPRESENTATION_CONTEXT ( 3 ) GLOBAL_UNCERTAINTY_ASSIGNED_CONTEXT ( ( #9914 ) ) GLOBAL_UNIT_ASSIGNED_CONTEXT ( ( #10354, #6966, #10451 ) ) REPRESENTATION_CONTEXT ( 'NONE', 'WORKASPACE' ) );
#6107=MECHANICAL_DESIGN_GEOMETRIC_PRESENTATION_REPRESENTATION('',(#13997),#5131);
#6111=PLANE ( 'NONE',  #11609 ) ;
#6142=EDGE_CURVE ( 'NONE', #7810, #11163, #19086, .T. ) ;
#6187=FILL_AREA_STYLE_COLOUR ( '', #1538 ) ;
#6204=DIRECTION ( 'NONE',  ( -1.000000000000000000, -0.000000000000000000, -0.000000000000000000 ) ) ;
#6207=LINE ( 'NONE', #7840, #16249 ) ;
#6209=( LENGTH_UNIT ( ) NAMED_UNIT ( * ) SI_UNIT ( .MILLI., .METRE. ) );
#6228=PLANE ( 'NONE',  #15313 ) ;
#6230=( NAMED_UNIT ( * ) SI_UNIT ( $, .STERADIAN. ) SOLID_ANGLE_UNIT ( ) );
#6260=DIRECTION ( 'NONE',  ( 1.000000000000000000, -0.000000000000000000, 0.000000000000000000 ) ) ;
#6262=( NAMED_UNIT ( * ) SI_UNIT ( $, .STERADIAN. ) SOLID_ANGLE_UNIT ( ) );
#6268=AXIS2_PLACEMENT_3D ( 'NONE', #14085, #15855, #4706 ) ;
#6329=ORIENTED_EDGE ( 'NONE', *, *, #18466, .F. ) ;
#6330=( LENGTH_UNIT ( ) NAMED_UNIT ( * ) SI_UNIT ( .MILLI., .METRE. ) );
#6338=VECTOR ( 'NONE', #80, 1000.000000000000000 ) ;
#6349=CYLINDRICAL_SURFACE ( 'NONE', #13532, 3.300000000000025135 ) ;
#6389=SURFACE_STYLE_USAGE ( .BOTH. , #4731 ) ;
#6401=ORIENTED_EDGE ( 'NONE', *, *, #17417, .T. ) ;
#6410=CARTESIAN_POINT ( 'NONE',  ( -75.00000000000000000, 368.2663108437010919, -142.2176018917206761 ) ) ;
#6415=PRESENTATION_STYLE_ASSIGNMENT (( #14225 ) ) ;
#6452=CARTESIAN_POINT ( 'NONE',  ( -75.00000000000000000, 368.2663108437010919, -142.2176018917206761 ) ) ;
#6485=FILL_AREA_STYLE_COLOUR ( '', #7578 ) ;
#6486=CARTESIAN_POINT ( 'NONE',  ( 10.00000000000000000, 381.0487089519826895, 2.719601036885452502E-12 ) ) ;
#6495=DIRECTION ( 'NONE',  ( 1.000000000000000000, 0.000000000000000000, 0.000000000000000000 ) ) ;
#6501=CARTESIAN_POINT ( 'NONE',  ( 10.00000000000000000, 372.8685141053778693, -83.18019484660869978 ) ) ;
#6512=SURFACE_STYLE_USAGE ( .BOTH. , #213 ) ;
#6521=VERTEX_POINT ( 'NONE', #5657 ) ;
#6538=( NAMED_UNIT ( * ) PLANE_ANGLE_UNIT ( ) SI_UNIT ( $, .RADIAN. ) );
#6543=ORIENTED_EDGE ( 'NONE', *, *, #4890, .F. ) ;
#6552=DIRECTION ( 'NONE',  ( 0.000000000000000000, 0.000000000000000000, -1.000000000000000000 ) ) ;
#6570=DIRECTION ( 'NONE',  ( -1.000000000000000000, -0.000000000000000000, -0.000000000000000000 ) ) ;
#6594=CARTESIAN_POINT ( 'NONE',  ( 10.00000000000000000, 381.0487089519837127, -150.0000000000032685 ) ) ;
#6601=( NAMED_UNIT ( * ) PLANE_ANGLE_UNIT ( ) SI_UNIT ( $, .RADIAN. ) );
#6604=EDGE_CURVE ( 'NONE', #11104, #14093, #3381, .T. ) ;
#6621=LINE ( 'NONE', #17731, #11011 ) ;
#6645=LINE ( 'NONE', #10131, #7214 ) ;
#6670=ORIENTED_EDGE ( 'NONE', *, *, #17199, .T. ) ;
#6703=VERTEX_POINT ( 'NONE', #3277 ) ;
#6712=CARTESIAN_POINT ( 'NONE',  ( 10.00000000000000000, 376.0487089519837127, -155.0000000000033253 ) ) ;
#6732=MECHANICAL_DESIGN_GEOMETRIC_PRESENTATION_REPRESENTATION('',(#1415),#14287);
#6757=SURFACE_STYLE_USAGE ( .BOTH. , #13046 ) ;
#6758=VERTEX_POINT ( 'NONE', #5742 ) ;
#6761=DIRECTION ( 'NONE',  ( 1.000000000000000000, 0.000000000000000000, 0.000000000000000000 ) ) ;
#6783=ORIENTED_EDGE ( 'NONE', *, *, #7142, .T. ) ;
#6803=CARTESIAN_POINT ( 'NONE',  ( -75.00000000000000000, 313.8311070602663904, -142.2176018917206761 ) ) ;
#6806=FACE_OUTER_BOUND ( 'NONE', #427, .T. ) ;
#6811=CARTESIAN_POINT ( 'NONE',  ( 10.00000000000000000, 309.2289037985890445, -150.1198051533984597 ) ) ;
#6820=ORIENTED_EDGE ( 'NONE', *, *, #4117, .F. ) ;
#6821=ORIENTED_EDGE ( 'NONE', *, *, #6920, .T. ) ;
#6874=DIRECTION ( 'NONE',  ( 0.000000000000000000, 0.000000000000000000, -1.000000000000000000 ) ) ;
#6900=STYLED_ITEM ( 'NONE', ( #11069 ), #4924 ) ;
#6920=EDGE_CURVE ( 'NONE', #6521, #10962, #17423, .T. ) ;
#6935=COLOUR_RGB ( '', 0.09019608, 0.27058824, 0.51372549) ;
#6949=EDGE_LOOP ( 'NONE', ( #17790, #227, #4378, #13234 ) ) ;
#6955=ORIENTED_EDGE ( 'NONE', *, *, #4971, .T. ) ;
#6966=( NAMED_UNIT ( * ) PLANE_ANGLE_UNIT ( ) SI_UNIT ( $, .RADIAN. ) );
#7006=EDGE_CURVE ( 'NONE', #14093, #3271, #1792, .T. ) ;
#7016=DIRECTION ( 'NONE',  ( 0.000000000000000000, 0.000000000000000000, -1.000000000000000000 ) ) ;
#7053=DIRECTION ( 'NONE',  ( -1.000000000000000000, -0.000000000000000000, -0.000000000000000000 ) ) ;
#7060=( GEOMETRIC_REPRESENTATION_CONTEXT ( 3 ) GLOBAL_UNCERTAINTY_ASSIGNED_CONTEXT ( ( #16447 ) ) GLOBAL_UNIT_ASSIGNED_CONTEXT ( ( #8201, #18789, #5115 ) ) REPRESENTATION_CONTEXT ( 'NONE', 'WORKASPACE' ) );
#7065=UNCERTAINTY_MEASURE_WITH_UNIT (LENGTH_MEASURE( 1.000000000000000082E-05 ), #17402, 'distance_accuracy_value', 'NONE');
#7076=FACE_BOUND ( 'NONE', #1724, .T. ) ;
#7077=LINE ( 'NONE', #13255, #11641 ) ;
#7142=EDGE_CURVE ( 'NONE', #19389, #7675, #15494, .T. ) ;
#7158=( NAMED_UNIT ( * ) PLANE_ANGLE_UNIT ( ) SI_UNIT ( $, .RADIAN. ) );
#7162=CARTESIAN_POINT ( 'NONE',  ( 0.000000000000000000, 0.000000000000000000, 0.000000000000000000 ) ) ;
#7177=SURFACE_STYLE_FILL_AREA ( #19913 ) ;
#7181=FACE_BOUND ( 'NONE', #19333, .T. ) ;
#7182=EDGE_LOOP ( 'NONE', ( #13108, #7464, #1081, #19792, #5167, #2916, #7668, #15582 ) ) ;
#7211=FILL_AREA_STYLE_COLOUR ( '', #13396 ) ;
#7214=VECTOR ( 'NONE', #1965, 1000.000000000000000 ) ;
#7238=ADVANCED_FACE ( 'NONE', ( #18515 ), #6349, .F. ) ;
#7247=EDGE_CURVE ( 'NONE', #10962, #6521, #1633, .T. ) ;
#7250=FACE_BOUND ( 'NONE', #16356, .T. ) ;
#7260=ORIENTED_EDGE ( 'NONE', *, *, #12733, .F. ) ;
#7271=LINE ( 'NONE', #14884, #5768 ) ;
#7274=FACE_OUTER_BOUND ( 'NONE', #7182, .T. ) ;
#7282=ORIENTED_EDGE ( 'NONE', *, *, #16245, .T. ) ;
#7290=CARTESIAN_POINT ( 'NONE',  ( 0.000000000000000000, 341.0487089519837696, -115.0000000000032969 ) ) ;
#7298=DIRECTION ( 'NONE',  ( 0.000000000000000000, 0.000000000000000000, 1.000000000000000000 ) ) ;
#7302=( LENGTH_UNIT ( ) NAMED_UNIT ( * ) SI_UNIT ( .MILLI., .METRE. ) );
#7325=DIRECTION ( 'NONE',  ( 0.000000000000000000, 0.000000000000000000, -1.000000000000000000 ) ) ;
#7348=FACE_BOUND ( 'NONE', #10158, .T. ) ;
#7350=COLOUR_RGB ( '', 0.72549020, 0.75294118, 0.79215686) ;
#7352=EDGE_LOOP ( 'NONE', ( #6783, #18586 ) ) ;
#7377=AXIS2_PLACEMENT_3D ( 'NONE', #6452, #4686, #18898 ) ;
#7394=CARTESIAN_POINT ( 'NONE',  ( 10.00000000000000000, 309.2289037985885898, -83.18019484660915452 ) ) ;
#7395=CARTESIAN_POINT ( 'NONE',  ( 10.00000000000000000, 372.8685141053783241, -150.1198051533980049 ) ) ;
#7400=FACE_OUTER_BOUND ( 'NONE', #16564, .T. ) ;
#7401=STYLED_ITEM ( 'NONE', ( #6415 ), #15054 ) ;
#7410=EDGE_LOOP ( 'NONE', ( #7533, #6329, #3082, #5033 ) ) ;
#7427=CARTESIAN_POINT ( 'NONE',  ( 0.000000000000000000, 309.2289037985885898, -79.88019484660914316 ) ) ;
#7430=SURFACE_STYLE_USAGE ( .BOTH. , #9067 ) ;
#7446=UNCERTAINTY_MEASURE_WITH_UNIT (LENGTH_MEASURE( 1.000000000000000082E-05 ), #19994, 'distance_accuracy_value', 'NONE');
#7450=( LENGTH_UNIT ( ) NAMED_UNIT ( * ) SI_UNIT ( .MILLI., .METRE. ) );
#7452=CARTESIAN_POINT ( 'NONE',  ( 10.00000000000000000, 381.0487089519832011, -80.00000000000332534 ) ) ;
#7456=AXIS2_PLACEMENT_3D ( 'NONE', #5171, #11444, #1735 ) ;
#7462=( NAMED_UNIT ( * ) SI_UNIT ( $, .STERADIAN. ) SOLID_ANGLE_UNIT ( ) );
#7464=ORIENTED_EDGE ( 'NONE', *, *, #6142, .T. ) ;
#7472=CARTESIAN_POINT ( 'NONE',  ( 0.000000000000000000, 372.8685141053783241, -143.5198051533979537 ) ) ;
#7507=CIRCLE ( 'NONE', #4214, 4.999999999999990230 ) ;
#7514=DIRECTION ( 'NONE',  ( 1.000000000000000000, -0.000000000000000000, 0.000000000000000000 ) ) ;
#7525=DIRECTION ( 'NONE',  ( 0.000000000000000000, 0.000000000000000000, 1.000000000000000000 ) ) ;
#7530=AXIS2_PLACEMENT_3D ( 'NONE', #7667, #18779, #3231 ) ;
#7533=ORIENTED_EDGE ( 'NONE', *, *, #18671, .T. ) ;
#7539=SURFACE_SIDE_STYLE ('',( #19883 ) ) ;
#7550=EDGE_LOOP ( 'NONE', ( #18651, #6401, #13461, #9150 ) ) ;
#7577=DIRECTION ( 'NONE',  ( 0.000000000000000000, -1.000000000000000000, -7.137148015447440312E-15 ) ) ;
#7578=COLOUR_RGB ( '', 0.66274510, 0.83137255, 0.94901961) ;
#7587=CARTESIAN_POINT ( 'NONE',  ( 10.00000000000000000, 376.0487089519831443, -75.00000000000331113 ) ) ;
#7622=ORIENTED_EDGE ( 'NONE', *, *, #8145, .F. ) ;
#7626=DIRECTION ( 'NONE',  ( 1.000000000000000000, -0.000000000000000000, -0.000000000000000000 ) ) ;
#7632=UNCERTAINTY_MEASURE_WITH_UNIT (LENGTH_MEASURE( 1.000000000000000082E-05 ), #9447, 'distance_accuracy_value', 'NONE');
#7667=CARTESIAN_POINT ( 'NONE',  ( 0.000000000000000000, 376.0487089519837127, -150.0000000000033538 ) ) ;
#7668=ORIENTED_EDGE ( 'NONE', *, *, #11280, .T. ) ;
#7675=VERTEX_POINT ( 'NONE', #1210 ) ;
#7701=EDGE_LOOP ( 'NONE', ( #3048, #1299, #8082, #12316 ) ) ;
#7718=( NAMED_UNIT ( * ) PLANE_ANGLE_UNIT ( ) SI_UNIT ( $, .RADIAN. ) );
#7723=MECHANICAL_DESIGN_GEOMETRIC_PRESENTATION_REPRESENTATION('',(#8397),#9689);
#7727=CARTESIAN_POINT ( 'NONE',  ( 0.000000000000000000, 368.2663108437010919, -142.2176018917206761 ) ) ;
#7729=EDGE_CURVE ( 'NONE', #2260, #13941, #363, .T. ) ;
#7744=SURFACE_STYLE_USAGE ( .BOTH. , #7539 ) ;
#7749=PLANE ( 'NONE',  #143 ) ;
#7776=FACE_OUTER_BOUND ( 'NONE', #13377, .T. ) ;
#7807=FILL_AREA_STYLE_COLOUR ( '', #13240 ) ;
#7810=VERTEX_POINT ( 'NONE', #6712 ) ;
#7831=ORIENTED_EDGE ( 'NONE', *, *, #11357, .F. ) ;
#7840=CARTESIAN_POINT ( 'NONE',  ( 0.000000000000000000, 381.0487089519826895, 2.719601036885452502E-12 ) ) ;
#7846=EDGE_CURVE ( 'NONE', #17086, #4537, #4067, .T. ) ;
#7866=ORIENTED_EDGE ( 'NONE', *, *, #7729, .T. ) ;
#7899=SURFACE_STYLE_FILL_AREA ( #1371 ) ;
#7901=ADVANCED_BREP_SHAPE_REPRESENTATION ( '', ( #1583, #2741 ), #19798 ) ;
#7906=( GEOMETRIC_REPRESENTATION_CONTEXT ( 3 ) GLOBAL_UNCERTAINTY_ASSIGNED_CONTEXT ( ( #13027 ) ) GLOBAL_UNIT_ASSIGNED_CONTEXT ( ( #4934, #14011, #1286 ) ) REPRESENTATION_CONTEXT ( 'NONE', 'WORKASPACE' ) );
#7913=EDGE_CURVE ( 'NONE', #8713, #1949, #5868, .T. ) ;
#7922=COLOUR_RGB ( '', 0.31764706, 0.68627451, 0.89019608) ;
#7942=FILL_AREA_STYLE_COLOUR ( '', #5432 ) ;
#7983=DIRECTION ( 'NONE',  ( 0.000000000000000000, 0.000000000000000000, -1.000000000000000000 ) ) ;
#8033=AXIS2_PLACEMENT_3D ( 'NONE', #14377, #1569, #7983 ) ;
#8035=PRESENTATION_STYLE_ASSIGNMENT (( #11324 ) ) ;
#8038=COLOUR_RGB ( '', 0.72549020, 0.75294118, 0.79215686) ;
#8052=CARTESIAN_POINT ( 'NONE',  ( -75.00000000000000000, 0.000000000000000000, 0.000000000000000000 ) ) ;
#8054=FILL_AREA_STYLE ('',( #1741 ) ) ;
#8082=ORIENTED_EDGE ( 'NONE', *, *, #6142, .F. ) ;
#8097=VERTEX_POINT ( 'NONE', #1386 ) ;
#8099=DIRECTION ( 'NONE',  ( 0.000000000000000000, 0.000000000000000000, 1.000000000000000000 ) ) ;
#8108=CARTESIAN_POINT ( 'NONE',  ( 10.00000000000000000, 372.8685141053783241, -146.8198051533979935 ) ) ;
#8111=DIRECTION ( 'NONE',  ( 1.000000000000000000, -0.000000000000000000, 0.000000000000000000 ) ) ;
#8118=PRESENTATION_STYLE_ASSIGNMENT (( #20263 ) ) ;
#8137=CARTESIAN_POINT ( 'NONE',  ( 0.000000000000000000, 313.8311070602663904, -87.78239810828596035 ) ) ;
#8145=EDGE_CURVE ( 'NONE', #7810, #10259, #9866, .T. ) ;
#8162=( LENGTH_UNIT ( ) NAMED_UNIT ( * ) SI_UNIT ( .MILLI., .METRE. ) );
#8201=( LENGTH_UNIT ( ) NAMED_UNIT ( * ) SI_UNIT ( .MILLI., .METRE. ) );
#8210=DIRECTION ( 'NONE',  ( 1.000000000000000000, -0.000000000000000000, 0.000000000000000000 ) ) ;
#8234=DIRECTION ( 'NONE',  ( 1.000000000000000000, 0.000000000000000000, 0.000000000000000000 ) ) ;
#8247=EDGE_LOOP ( 'NONE', ( #10609, #7866, #13856, #10400 ) ) ;
#8267=UNCERTAINTY_MEASURE_WITH_UNIT (LENGTH_MEASURE( 1.000000000000000082E-05 ), #7302, 'distance_accuracy_value', 'NONE');
#8285=( LENGTH_UNIT ( ) NAMED_UNIT ( * ) SI_UNIT ( .MILLI., .METRE. ) );
#8320=COLOUR_RGB ( '', 0.09019608, 0.27058824, 0.51372549) ;
#8353=DIRECTION ( 'NONE',  ( 0.000000000000000000, 0.000000000000000000, -1.000000000000000000 ) ) ;
#8355=DIRECTION ( 'NONE',  ( 0.000000000000000000, 0.000000000000000000, -1.000000000000000000 ) ) ;
#8397=STYLED_ITEM ( 'NONE', ( #11876 ), #1583 ) ;
#8404=VECTOR ( 'NONE', #9667, 1000.000000000000000 ) ;
#8442=FILL_AREA_STYLE_COLOUR ( '', #6057 ) ;
#8444=CIRCLE ( 'NONE', #17962, 3.300000000000025135 ) ;
#8456=CYLINDRICAL_SURFACE ( 'NONE', #16375, 3.300000000000011369 ) ;
#8472=UNCERTAINTY_MEASURE_WITH_UNIT (LENGTH_MEASURE( 1.000000000000000082E-05 ), #10032, 'distance_accuracy_value', 'NONE');
#8507=ORIENTED_EDGE ( 'NONE', *, *, #16115, .T. ) ;
#8509=ORIENTED_EDGE ( 'NONE', *, *, #2690, .F. ) ;
#8539=DIRECTION ( 'NONE',  ( 1.000000000000000000, -0.000000000000000000, 0.000000000000000000 ) ) ;
#8549=DIRECTION ( 'NONE',  ( -0.000000000000000000, -1.000000000000000000, -0.000000000000000000 ) ) ;
#8567=FACE_OUTER_BOUND ( 'NONE', #15884, .T. ) ;
#8613=EDGE_LOOP ( 'NONE', ( #3375, #10637, #12690, #19620 ) ) ;
#8614=FILL_AREA_STYLE_COLOUR ( '', #19882 ) ;
#8617=AXIS2_PLACEMENT_3D ( 'NONE', #5204, #16241, #15931 ) ;
#8640=ORIENTED_EDGE ( 'NONE', *, *, #1901, .F. ) ;
#8664=DIRECTION ( 'NONE',  ( 1.000000000000000000, -0.000000000000000000, 0.000000000000000000 ) ) ;
#8665=UNCERTAINTY_MEASURE_WITH_UNIT (LENGTH_MEASURE( 1.000000000000000082E-05 ), #5784, 'distance_accuracy_value', 'NONE');
#8684=( NAMED_UNIT ( * ) SI_UNIT ( $, .STERADIAN. ) SOLID_ANGLE_UNIT ( ) );
#8693=VECTOR ( 'NONE', #9685, 1000.000000000000000 ) ;
#8711=FACE_OUTER_BOUND ( 'NONE', #17581, .T. ) ;
#8713=VERTEX_POINT ( 'NONE', #5331 ) ;
#8725=COLOUR_RGB ( '', 0.08235294, 0.09019608, 0.10196078) ;
#8731=DIRECTION ( 'NONE',  ( 0.000000000000000000, 0.000000000000000000, -1.000000000000000000 ) ) ;
#8741=EDGE_CURVE ( 'NONE', #9449, #19389, #18568, .T. ) ;
#8749=FILL_AREA_STYLE ('',( #8843 ) ) ;
#8839=( NAMED_UNIT ( * ) SI_UNIT ( $, .STERADIAN. ) SOLID_ANGLE_UNIT ( ) );
#8843=FILL_AREA_STYLE_COLOUR ( '', #13504 ) ;
#8846=PRODUCT_DEFINITION_CONTEXT ( 'detailed design', #16595, 'design' ) ;
#8863=VECTOR ( 'NONE', #18908, 1000.000000000000000 ) ;
#8880=PLANE ( 'NONE',  #19567 ) ;
#8913=EDGE_LOOP ( 'NONE', ( #5499, #5620, #15787, #9145 ) ) ;
#8919=CARTESIAN_POINT ( 'NONE',  ( 10.00000000000000000, 372.8685141053778693, -79.88019484660868841 ) ) ;
#8924=PRESENTATION_STYLE_ASSIGNMENT (( #10781 ) ) ;
#8940=FILL_AREA_STYLE ('',( #14378 ) ) ;
#8968=( GEOMETRIC_REPRESENTATION_CONTEXT ( 3 ) GLOBAL_UNCERTAINTY_ASSIGNED_CONTEXT ( ( #15479 ) ) GLOBAL_UNIT_ASSIGNED_CONTEXT ( ( #11285, #5133, #462 ) ) REPRESENTATION_CONTEXT ( 'NONE', 'WORKASPACE' ) );
#8970=CYLINDRICAL_SURFACE ( 'NONE', #19284, 5.000000000000004441 ) ;
#8979=LINE ( 'NONE', #6486, #6338 ) ;
#8984=( NAMED_UNIT ( * ) PLANE_ANGLE_UNIT ( ) SI_UNIT ( $, .RADIAN. ) );
#9014=ORIENTED_EDGE ( 'NONE', *, *, #5076, .T. ) ;
#9015=( GEOMETRIC_REPRESENTATION_CONTEXT ( 3 ) GLOBAL_UNCERTAINTY_ASSIGNED_CONTEXT ( ( #14855 ) ) GLOBAL_UNIT_ASSIGNED_CONTEXT ( ( #14718, #15023, #12041 ) ) REPRESENTATION_CONTEXT ( 'NONE', 'WORKASPACE' ) );
#9029=SURFACE_STYLE_FILL_AREA ( #4598 ) ;
#9036=DIRECTION ( 'NONE',  ( 0.000000000000000000, -7.137148015447440312E-15, 1.000000000000000000 ) ) ;
#9038=PRESENTATION_STYLE_ASSIGNMENT (( #13771 ) ) ;
#9067=SURFACE_SIDE_STYLE ('',( #15250 ) ) ;
#9074=( NAMED_UNIT ( * ) PLANE_ANGLE_UNIT ( ) SI_UNIT ( $, .RADIAN. ) );
#9075=VECTOR ( 'NONE', #10217, 1000.000000000000000 ) ;
#9131=FILL_AREA_STYLE ('',( #19934 ) ) ;
#9134=DIRECTION ( 'NONE',  ( -1.000000000000000000, -0.000000000000000000, -0.000000000000000000 ) ) ;
#9145=ORIENTED_EDGE ( 'NONE', *, *, #18214, .F. ) ;
#9148=EDGE_LOOP ( 'NONE', ( #13558, #16893, #8640, #13202 ) ) ;
#9150=ORIENTED_EDGE ( 'NONE', *, *, #1020, .F. ) ;
#9156=SURFACE_STYLE_FILL_AREA ( #2860 ) ;
#9162=EDGE_CURVE ( 'NONE', #12228, #9449, #8444, .T. ) ;
#9214=EDGE_LOOP ( 'NONE', ( #16784, #1500, #5570, #17020, #15419, #9908, #9375, #6543 ) ) ;
#9234=FACE_OUTER_BOUND ( 'NONE', #7550, .T. ) ;
#9248=AXIS2_PLACEMENT_3D ( 'NONE', #16166, #1993, #6083 ) ;
#9254=PRESENTATION_STYLE_ASSIGNMENT (( #7430 ) ) ;
#9256=PRESENTATION_STYLE_ASSIGNMENT (( #6389 ) ) ;
#9298=ORIENTED_EDGE ( 'NONE', *, *, #14794, .T. ) ;
#9324=SURFACE_STYLE_FILL_AREA ( #1670 ) ;
#9330=DIRECTION ( 'NONE',  ( -1.000000000000000000, -0.000000000000000000, -0.000000000000000000 ) ) ;
#9375=ORIENTED_EDGE ( 'NONE', *, *, #3577, .F. ) ;
#9397=CARTESIAN_POINT ( 'NONE',  ( 10.00000000000000000, 381.0487089519826895, 2.719601036885452502E-12 ) ) ;
#9447=( LENGTH_UNIT ( ) NAMED_UNIT ( * ) SI_UNIT ( .MILLI., .METRE. ) );
#9449=VERTEX_POINT ( 'NONE', #1730 ) ;
#9473=PLANE ( 'NONE',  #20210 ) ;
#9491=AXIS2_PLACEMENT_3D ( 'NONE', #3330, #4672, #10857 ) ;
#9500=DIRECTION ( 'NONE',  ( 0.000000000000000000, -1.000000000000000000, -7.137148015447440312E-15 ) ) ;
#9510=SURFACE_STYLE_FILL_AREA ( #1870 ) ;
#9523=CARTESIAN_POINT ( 'NONE',  ( 0.000000000000000000, 341.0487089519837696, -115.0000000000032969 ) ) ;
#9539=SURFACE_SIDE_STYLE ('',( #7899 ) ) ;
#9569=VECTOR ( 'NONE', #19264, 1000.000000000000000 ) ;
#9578=ADVANCED_FACE ( 'NONE', ( #13203 ), #8456, .F. ) ;
#9592=EDGE_LOOP ( 'NONE', ( #10568, #18362, #10997, #1861 ) ) ;
#9640=SHAPE_REPRESENTATION_RELATIONSHIP ( 'NONE' , 'NONE' ,  #10923, #7901 ) ;
#9641=FACE_OUTER_BOUND ( 'NONE', #15719, .T. ) ;
#9647=ORIENTED_EDGE ( 'NONE', *, *, #3577, .T. ) ;
#9654=VECTOR ( 'NONE', #13809, 1000.000000000000000 ) ;
#9662=LINE ( 'NONE', #8137, #11454 ) ;
#9667=DIRECTION ( 'NONE',  ( -1.000000000000000000, -0.000000000000000000, -0.000000000000000000 ) ) ;
#9685=DIRECTION ( 'NONE',  ( 1.000000000000000000, -0.000000000000000000, -0.000000000000000000 ) ) ;
#9689=( GEOMETRIC_REPRESENTATION_CONTEXT ( 3 ) GLOBAL_UNCERTAINTY_ASSIGNED_CONTEXT ( ( #5818 ) ) GLOBAL_UNIT_ASSIGNED_CONTEXT ( ( #7450, #18134, #18248 ) ) REPRESENTATION_CONTEXT ( 'NONE', 'WORKASPACE' ) );
#9696=CARTESIAN_POINT ( 'NONE',  ( 0.000000000000000000, 376.0487089519831443, -75.00000000000331113 ) ) ;
#9705=AXIS2_PLACEMENT_3D ( 'NONE', #18336, #10204, #2673 ) ;
#9707=VECTOR ( 'NONE', #5338, 1000.000000000000000 ) ;
#9768=EDGE_CURVE ( 'NONE', #140, #5163, #15366, .T. ) ;
#9799=( GEOMETRIC_REPRESENTATION_CONTEXT ( 3 ) GLOBAL_UNCERTAINTY_ASSIGNED_CONTEXT ( ( #14686 ) ) GLOBAL_UNIT_ASSIGNED_CONTEXT ( ( #10498, #17089, #10916 ) ) REPRESENTATION_CONTEXT ( 'NONE', 'WORKASPACE' ) );
#9832=VERTEX_POINT ( 'NONE', #5235 ) ;
#9866=LINE ( 'NONE', #5146, #12587 ) ;
#9879=LINE ( 'NONE', #10279, #17093 ) ;
#9908=ORIENTED_EDGE ( 'NONE', *, *, #18671, .F. ) ;
#9914=UNCERTAINTY_MEASURE_WITH_UNIT (LENGTH_MEASURE( 1.000000000000000082E-05 ), #10354, 'distance_accuracy_value', 'NONE');
#10008=EDGE_CURVE ( 'NONE', #18431, #6703, #12317, .T. ) ;
#10017=CIRCLE ( 'NONE', #16616, 3.300000000000011369 ) ;
#10027=AXIS2_PLACEMENT_3D ( 'NONE', #7162, #12179, #18454 ) ;
#10032=( LENGTH_UNIT ( ) NAMED_UNIT ( * ) SI_UNIT ( .MILLI., .METRE. ) );
#10037=DIRECTION ( 'NONE',  ( 0.000000000000000000, 0.000000000000000000, -1.000000000000000000 ) ) ;
#10042=ORIENTED_EDGE ( 'NONE', *, *, #10117, .F. ) ;
#10045=VERTEX_POINT ( 'NONE', #5735 ) ;
#10117=EDGE_CURVE ( 'NONE', #9449, #12228, #10338, .T. ) ;
#10121=ORIENTED_EDGE ( 'NONE', *, *, #10982, .T. ) ;
#10123=FILL_AREA_STYLE_COLOUR ( '', #16629 ) ;
#10131=CARTESIAN_POINT ( 'NONE',  ( 0.000000000000000000, 313.8311070602663904, -142.2176018917206761 ) ) ;
#10139=ADVANCED_FACE ( 'NONE', ( #1882 ), #12625, .F. ) ;
#10155=DIRECTION ( 'NONE',  ( 1.000000000000000000, -0.000000000000000000, -0.000000000000000000 ) ) ;
#10158=EDGE_LOOP ( 'NONE', ( #14150, #12550 ) ) ;
#10159=ORIENTED_EDGE ( 'NONE', *, *, #288, .F. ) ;
#10170=CARTESIAN_POINT ( 'NONE',  ( 0.000000000000000000, 306.0487089519832011, -80.00000000000380851 ) ) ;
#10204=DIRECTION ( 'NONE',  ( 1.000000000000000000, -0.000000000000000000, 0.000000000000000000 ) ) ;
#10207=AXIS2_PLACEMENT_3D ( 'NONE', #13375, #12015, #19614 ) ;
#10215=SURFACE_STYLE_USAGE ( .BOTH. , #5891 ) ;
#10217=DIRECTION ( 'NONE',  ( 0.000000000000000000, 1.000000000000000000, 7.137148015447440312E-15 ) ) ;
#10220=SURFACE_STYLE_FILL_AREA ( #10436 ) ;
#10253=STYLED_ITEM ( 'NONE', ( #8118 ), #17573 ) ;
#10259=VERTEX_POINT ( 'NONE', #15393 ) ;
#10271=DIRECTION ( 'NONE',  ( 0.000000000000000000, 0.000000000000000000, -1.000000000000000000 ) ) ;
#10279=CARTESIAN_POINT ( 'NONE',  ( 0.000000000000000000, 313.8311070602663904, -142.2176018917206761 ) ) ;
#10285=ORIENTED_EDGE ( 'NONE', *, *, #10810, .T. ) ;
#10332=VECTOR ( 'NONE', #20100, 1000.000000000000000 ) ;
#10333=CARTESIAN_POINT ( 'NONE',  ( 10.00000000000000000, 301.0487089519837127, -150.0000000000038369 ) ) ;
#10334=VECTOR ( 'NONE', #15043, 1000.000000000000000 ) ;
#10338=CIRCLE ( 'NONE', #8033, 3.300000000000025135 ) ;
#10340=VERTEX_POINT ( 'NONE', #10746 ) ;
#10353=MECHANICAL_DESIGN_GEOMETRIC_PRESENTATION_REPRESENTATION('',(#15975),#19538);
#10354=( LENGTH_UNIT ( ) NAMED_UNIT ( * ) SI_UNIT ( .MILLI., .METRE. ) );
#10374=SURFACE_STYLE_USAGE ( .BOTH. , #18386 ) ;
#10400=ORIENTED_EDGE ( 'NONE', *, *, #18011, .F. ) ;
#10436=FILL_AREA_STYLE ('',( #15170 ) ) ;
#10441=PRESENTATION_STYLE_ASSIGNMENT (( #13827 ) ) ;
#10451=( NAMED_UNIT ( * ) SI_UNIT ( $, .STERADIAN. ) SOLID_ANGLE_UNIT ( ) );
#10463=ORIENTED_EDGE ( 'NONE', *, *, #2833, .T. ) ;
#10466=CIRCLE ( 'NONE', #2211, 3.300000000000011369 ) ;
#10469=DIRECTION ( 'NONE',  ( 0.000000000000000000, 0.000000000000000000, -1.000000000000000000 ) ) ;
#10471=( LENGTH_UNIT ( ) NAMED_UNIT ( * ) SI_UNIT ( .MILLI., .METRE. ) );
#10477=CARTESIAN_POINT ( 'NONE',  ( 10.00000000000000000, 376.0487089519831443, -75.00000000000331113 ) ) ;
#10498=( LENGTH_UNIT ( ) NAMED_UNIT ( * ) SI_UNIT ( .MILLI., .METRE. ) );
#10504=DIRECTION ( 'NONE',  ( -1.000000000000000000, -0.000000000000000000, -0.000000000000000000 ) ) ;
#10508=COLOUR_RGB ( '', 0.31764706, 0.68627451, 0.89019608) ;
#10535=SURFACE_SIDE_STYLE ('',( #4256 ) ) ;
#10538=ORIENTED_EDGE ( 'NONE', *, *, #9162, .F. ) ;
#10557=FACE_BOUND ( 'NONE', #17671, .T. ) ;
#10568=ORIENTED_EDGE ( 'NONE', *, *, #10117, .T. ) ;
#10574=CARTESIAN_POINT ( 'NONE',  ( 10.00000000000000000, 306.0487089519837127, -150.0000000000038369 ) ) ;
#10600=DIRECTION ( 'NONE',  ( -1.000000000000000000, -0.000000000000000000, -0.000000000000000000 ) ) ;
#10604=PRESENTATION_STYLE_ASSIGNMENT (( #13796 ) ) ;
#10609=ORIENTED_EDGE ( 'NONE', *, *, #17417, .F. ) ;
#10637=ORIENTED_EDGE ( 'NONE', *, *, #2695, .T. ) ;
#10652=ORIENTED_EDGE ( 'NONE', *, *, #6604, .F. ) ;
#10654=SHAPE_DEFINITION_REPRESENTATION ( #20088, #10923 ) ;
#10668=VERTEX_POINT ( 'NONE', #10913 ) ;
#10675=DIRECTION ( 'NONE',  ( -1.000000000000000000, -0.000000000000000000, -0.000000000000000000 ) ) ;
#10681=( GEOMETRIC_REPRESENTATION_CONTEXT ( 3 ) GLOBAL_UNCERTAINTY_ASSIGNED_CONTEXT ( ( #2058 ) ) GLOBAL_UNIT_ASSIGNED_CONTEXT ( ( #8285, #14360, #17539 ) ) REPRESENTATION_CONTEXT ( 'NONE', 'WORKASPACE' ) );
#10702=DIRECTION ( 'NONE',  ( 0.000000000000000000, 0.000000000000000000, -1.000000000000000000 ) ) ;
#10707=FILL_AREA_STYLE_COLOUR ( '', #5813 ) ;
#10708=VECTOR ( 'NONE', #9500, 1000.000000000000000 ) ;
#10721=MECHANICAL_DESIGN_GEOMETRIC_PRESENTATION_REPRESENTATION('',(#16023),#3830);
#10746=CARTESIAN_POINT ( 'NONE',  ( 10.00000000000000000, 309.2289037985885898, -86.48019484660916589 ) ) ;
#10781=SURFACE_STYLE_USAGE ( .BOTH. , #13679 ) ;
#10810=EDGE_CURVE ( 'NONE', #3271, #12099, #19528, .T. ) ;
#10857=DIRECTION ( 'NONE',  ( 0.000000000000000000, 0.000000000000000000, 1.000000000000000000 ) ) ;
#10883=ADVANCED_FACE ( 'NONE', ( #5938 ), #12328, .T. ) ;
#10913=CARTESIAN_POINT ( 'NONE',  ( 10.00000000000000000, 341.0487089519837696, -133.5000000000032969 ) ) ;
#10916=( NAMED_UNIT ( * ) SI_UNIT ( $, .STERADIAN. ) SOLID_ANGLE_UNIT ( ) );
#10923=SHAPE_REPRESENTATION ( 'Part4', ( #2741 ), #19798 ) ;
#10933=ORIENTED_EDGE ( 'NONE', *, *, #431, .F. ) ;
#10940=DIRECTION ( 'NONE',  ( 1.000000000000000000, -0.000000000000000000, 0.000000000000000000 ) ) ;
#10962=VERTEX_POINT ( 'NONE', #14075 ) ;
#10982=EDGE_CURVE ( 'NONE', #14093, #10045, #10983, .T. ) ;
#10983=LINE ( 'NONE', #17271, #8863 ) ;
#10994=CARTESIAN_POINT ( 'NONE',  ( 10.00000000000000000, 372.8685141053778693, -83.18019484660869978 ) ) ;
#10997=ORIENTED_EDGE ( 'NONE', *, *, #7142, .F. ) ;
#10999=( GEOMETRIC_REPRESENTATION_CONTEXT ( 3 ) GLOBAL_UNCERTAINTY_ASSIGNED_CONTEXT ( ( #17736 ) ) GLOBAL_UNIT_ASSIGNED_CONTEXT ( ( #637, #19485, #8684 ) ) REPRESENTATION_CONTEXT ( 'NONE', 'WORKASPACE' ) );
#11011=VECTOR ( 'NONE', #8549, 1000.000000000000000 ) ;
#11012=MECHANICAL_DESIGN_GEOMETRIC_PRESENTATION_REPRESENTATION('',(#7401),#16944);
#11069=PRESENTATION_STYLE_ASSIGNMENT (( #14250 ) ) ;
#11080=ORIENTED_EDGE ( 'NONE', *, *, #8741, .T. ) ;
#11095=CYLINDRICAL_SURFACE ( 'NONE', #16858, 3.300000000000011369 ) ;
#11104=VERTEX_POINT ( 'NONE', #16952 ) ;
#11126=LINE ( 'NONE', #1930, #8693 ) ;
#11134=( NAMED_UNIT ( * ) SI_UNIT ( $, .STERADIAN. ) SOLID_ANGLE_UNIT ( ) );
#11140=CARTESIAN_POINT ( 'NONE',  ( 0.000000000000000000, 309.2289037985890445, -143.5198051533984085 ) ) ;
#11141=MECHANICAL_DESIGN_GEOMETRIC_PRESENTATION_REPRESENTATION('',(#6900),#11480);
#11159=FILL_AREA_STYLE_COLOUR ( '', #17391 ) ;
#11163=VERTEX_POINT ( 'NONE', #231 ) ;
#11178=SURFACE_SIDE_STYLE ('',( #16897 ) ) ;
#11189=( NAMED_UNIT ( * ) PLANE_ANGLE_UNIT ( ) SI_UNIT ( $, .RADIAN. ) );
#11225=DIRECTION ( 'NONE',  ( 0.000000000000000000, 0.000000000000000000, -1.000000000000000000 ) ) ;
#11229=EDGE_LOOP ( 'NONE', ( #15035, #6821 ) ) ;
#11231=DIRECTION ( 'NONE',  ( 0.000000000000000000, 0.000000000000000000, -1.000000000000000000 ) ) ;
#11233=SURFACE_STYLE_FILL_AREA ( #8054 ) ;
#11246=CARTESIAN_POINT ( 'NONE',  ( 10.00000000000000000, 376.0487089519837127, -150.0000000000033538 ) ) ;
#11280=EDGE_CURVE ( 'NONE', #548, #6758, #17536, .T. ) ;
#11285=( LENGTH_UNIT ( ) NAMED_UNIT ( * ) SI_UNIT ( .MILLI., .METRE. ) );
#11291=LINE ( 'NONE', #3673, #3687 ) ;
#11324=SURFACE_STYLE_USAGE ( .BOTH. , #1726 ) ;
#11327=CIRCLE ( 'NONE', #11997, 3.300000000000025135 ) ;
#11348=MECHANICAL_DESIGN_GEOMETRIC_PRESENTATION_REPRESENTATION('',(#2127),#3457);
#11349=MECHANICAL_DESIGN_GEOMETRIC_PRESENTATION_REPRESENTATION('',(#20224),#17759);
#11357=EDGE_CURVE ( 'NONE', #867, #6703, #3132, .T. ) ;
#11360=UNCERTAINTY_MEASURE_WITH_UNIT (LENGTH_MEASURE( 1.000000000000000082E-05 ), #17025, 'distance_accuracy_value', 'NONE');
#11363=LINE ( 'NONE', #4876, #10708 ) ;
#11444=DIRECTION ( 'NONE',  ( 1.000000000000000000, -0.000000000000000000, 0.000000000000000000 ) ) ;
#11454=VECTOR ( 'NONE', #17299, 1000.000000000000000 ) ;
#11470=AXIS2_PLACEMENT_3D ( 'NONE', #14176, #8111, #3038 ) ;
#11479=CARTESIAN_POINT ( 'NONE',  ( 10.00000000000000000, 309.2289037985890445, -146.8198051533984199 ) ) ;
#11480=( GEOMETRIC_REPRESENTATION_CONTEXT ( 3 ) GLOBAL_UNCERTAINTY_ASSIGNED_CONTEXT ( ( #11583 ) ) GLOBAL_UNIT_ASSIGNED_CONTEXT ( ( #6330, #6538, #6230 ) ) REPRESENTATION_CONTEXT ( 'NONE', 'WORKASPACE' ) );
#11536=CARTESIAN_POINT ( 'NONE',  ( 10.00000000000000000, 309.2289037985885898, -83.18019484660915452 ) ) ;
#11540=STYLED_ITEM ( 'NONE', ( #9256 ), #16712 ) ;
#11542=STYLED_ITEM ( 'NONE', ( #19956 ), #7238 ) ;
#11561=UNCERTAINTY_MEASURE_WITH_UNIT (LENGTH_MEASURE( 1.000000000000000082E-05 ), #6209, 'distance_accuracy_value', 'NONE');
#11563=DIRECTION ( 'NONE',  ( 1.000000000000000000, -0.000000000000000000, 0.000000000000000000 ) ) ;
#11583=UNCERTAINTY_MEASURE_WITH_UNIT (LENGTH_MEASURE( 1.000000000000000082E-05 ), #6330, 'distance_accuracy_value', 'NONE');
#11600=ORIENTED_EDGE ( 'NONE', *, *, #1655, .T. ) ;
#11609=AXIS2_PLACEMENT_3D ( 'NONE', #9397, #4452, #4653 ) ;
#11628=AXIS2_PLACEMENT_3D ( 'NONE', #12044, #9036, #4209 ) ;
#11641=VECTOR ( 'NONE', #14586, 1000.000000000000000 ) ;
#11680=PRESENTATION_STYLE_ASSIGNMENT (( #5497 ) ) ;
#11683=PRESENTATION_STYLE_ASSIGNMENT (( #14984 ) ) ;
#11690=ORIENTED_EDGE ( 'NONE', *, *, #9768, .T. ) ;
#11703=CIRCLE ( 'NONE', #9705, 5.000000000000004441 ) ;
#11712=CARTESIAN_POINT ( 'NONE',  ( 10.00000000000000000, 1.106257942394396377E-12, -155.0000000000060254 ) ) ;
#11780=CARTESIAN_POINT ( 'NONE',  ( 0.000000000000000000, 1.106257942394396377E-12, -155.0000000000060254 ) ) ;
#11849=DIRECTION ( 'NONE',  ( 0.000000000000000000, 0.000000000000000000, 1.000000000000000000 ) ) ;
#11876=PRESENTATION_STYLE_ASSIGNMENT (( #10215 ) ) ;
#11928=DIRECTION ( 'NONE',  ( 0.000000000000000000, 0.000000000000000000, 1.000000000000000000 ) ) ;
#11931=( NAMED_UNIT ( * ) PLANE_ANGLE_UNIT ( ) SI_UNIT ( $, .RADIAN. ) );
#11990=STYLED_ITEM ( 'NONE', ( #11683 ), #15608 ) ;
#11993=ORIENTED_EDGE ( 'NONE', *, *, #2695, .F. ) ;
#11997=AXIS2_PLACEMENT_3D ( 'NONE', #8108, #14695, #6874 ) ;
#12003=CARTESIAN_POINT ( 'NONE',  ( 0.000000000000000000, 372.8685141053778693, -86.48019484660871115 ) ) ;
#12010=EDGE_CURVE ( 'NONE', #13941, #2260, #3322, .T. ) ;
#12013=ORIENTED_EDGE ( 'NONE', *, *, #16115, .F. ) ;
#12015=DIRECTION ( 'NONE',  ( 1.000000000000000000, -0.000000000000000000, 0.000000000000000000 ) ) ;
#12020=ORIENTED_EDGE ( 'NONE', *, *, #17679, .F. ) ;
#12041=( NAMED_UNIT ( * ) SI_UNIT ( $, .STERADIAN. ) SOLID_ANGLE_UNIT ( ) );
#12044=CARTESIAN_POINT ( 'NONE',  ( 10.00000000000000000, 1.106257942394396377E-12, -155.0000000000060254 ) ) ;
#12046=PLANE ( 'NONE',  #2457 ) ;
#12099=VERTEX_POINT ( 'NONE', #20060 ) ;
#12106=FACE_BOUND ( 'NONE', #19509, .T. ) ;
#12120=CYLINDRICAL_SURFACE ( 'NONE', #2030, 5.000000000000004441 ) ;
#12125=LINE ( 'NONE', #10477, #15926 ) ;
#12127=SURFACE_STYLE_FILL_AREA ( #2330 ) ;
#12160=AXIS2_PLACEMENT_3D ( 'NONE', #2934, #9330, #4388 ) ;
#12179=DIRECTION ( 'NONE',  ( 1.000000000000000000, -0.000000000000000000, 0.000000000000000000 ) ) ;
#12213=FACE_OUTER_BOUND ( 'NONE', #9148, .T. ) ;
#12228=VERTEX_POINT ( 'NONE', #1827 ) ;
#12242=CYLINDRICAL_SURFACE ( 'NONE', #3711, 3.300000000000011369 ) ;
#12252=CARTESIAN_POINT ( 'NONE',  ( 10.00000000000000000, 306.0487089519832011, -80.00000000000380851 ) ) ;
#12316=ORIENTED_EDGE ( 'NONE', *, *, #8145, .T. ) ;
#12317=LINE ( 'NONE', #13972, #3756 ) ;
#12320=DIRECTION ( 'NONE',  ( 1.000000000000000000, -0.000000000000000000, -0.000000000000000000 ) ) ;
#12323=STYLED_ITEM ( 'NONE', ( #18488 ), #930 ) ;
#12326=SURFACE_SIDE_STYLE ('',( #18390 ) ) ;
#12328=CYLINDRICAL_SURFACE ( 'NONE', #12160, 5.000000000000004441 ) ;
#12339=AXIS2_PLACEMENT_3D ( 'NONE', #4141, #18529, #4235 ) ;
#12371=ADVANCED_FACE ( 'NONE', ( #6806 ), #19133, .F. ) ;
#12385=DIRECTION ( 'NONE',  ( 0.000000000000000000, 0.000000000000000000, 1.000000000000000000 ) ) ;
#12496=DIRECTION ( 'NONE',  ( -1.000000000000000000, -0.000000000000000000, -0.000000000000000000 ) ) ;
#12505=FILL_AREA_STYLE_COLOUR ( '', #1781 ) ;
#12523=PRESENTATION_STYLE_ASSIGNMENT (( #15941 ) ) ;
#12550=ORIENTED_EDGE ( 'NONE', *, *, #18214, .T. ) ;
#12562=FACE_OUTER_BOUND ( 'NONE', #30, .T. ) ;
#12565=DIRECTION ( 'NONE',  ( -0.000000000000000000, -0.000000000000000000, -1.000000000000000000 ) ) ;
#12574=EDGE_CURVE ( 'NONE', #8097, #4515, #11327, .T. ) ;
#12587=VECTOR ( 'NONE', #17892, 1000.000000000000000 ) ;
#12610=MECHANICAL_DESIGN_GEOMETRIC_PRESENTATION_REPRESENTATION('',(#18845),#5048);
#12625=PLANE ( 'NONE',  #7377 ) ;
#12671=ADVANCED_FACE ( 'NONE', ( #8711 ), #15003, .F. ) ;
#12690=ORIENTED_EDGE ( 'NONE', *, *, #19508, .T. ) ;
#12733=EDGE_CURVE ( 'NONE', #1663, #140, #7271, .T. ) ;
#12743=SURFACE_SIDE_STYLE ('',( #9324 ) ) ;
#12796=DIRECTION ( 'NONE',  ( -0.000000000000000000, -0.000000000000000000, -1.000000000000000000 ) ) ;
#12825=DIRECTION ( 'NONE',  ( -1.000000000000000000, -0.000000000000000000, -0.000000000000000000 ) ) ;
#12834=VECTOR ( 'NONE', #2643, 1000.000000000000000 ) ;
#12858=ORIENTED_EDGE ( 'NONE', *, *, #12733, .T. ) ;
#12877=PRESENTATION_STYLE_ASSIGNMENT (( #3690 ) ) ;
#12909=ADVANCED_FACE ( 'NONE', ( #7776 ), #6228, .F. ) ;
#12930=DIRECTION ( 'NONE',  ( -1.000000000000000000, 0.000000000000000000, -0.000000000000000000 ) ) ;
#12951=AXIS2_PLACEMENT_3D ( 'NONE', #5894, #10940, #18448 ) ;
#13007=CARTESIAN_POINT ( 'NONE',  ( 10.00000000000000000, 376.0487089519832011, -80.00000000000332534 ) ) ;
#13027=UNCERTAINTY_MEASURE_WITH_UNIT (LENGTH_MEASURE( 1.000000000000000082E-05 ), #4934, 'distance_accuracy_value', 'NONE');
#13046=SURFACE_SIDE_STYLE ('',( #5199 ) ) ;
#13061=ADVANCED_FACE ( 'NONE', ( #8567 ), #8880, .F. ) ;
#13097=CARTESIAN_POINT ( 'NONE',  ( -75.00000000000000000, 368.2663108437010919, -87.78239810828596035 ) ) ;
#13098=SURFACE_SIDE_STYLE ('',( #4932 ) ) ;
#13108=ORIENTED_EDGE ( 'NONE', *, *, #4688, .T. ) ;
#13130=DIRECTION ( 'NONE',  ( 0.000000000000000000, 0.000000000000000000, -1.000000000000000000 ) ) ;
#13200=ORIENTED_EDGE ( 'NONE', *, *, #4552, .T. ) ;
#13202=ORIENTED_EDGE ( 'NONE', *, *, #19234, .T. ) ;
#13203=FACE_OUTER_BOUND ( 'NONE', #5916, .T. ) ;
#13204=CARTESIAN_POINT ( 'NONE',  ( 10.00000000000000000, 301.0487089519832011, -80.00000000000387956 ) ) ;
#13213=EDGE_CURVE ( 'NONE', #11163, #17086, #8979, .T. ) ;
#13234=ORIENTED_EDGE ( 'NONE', *, *, #11357, .T. ) ;
#13240=COLOUR_RGB ( '', 0.40784314, 0.44705882, 0.49803922) ;
#13242=ORIENTED_EDGE ( 'NONE', *, *, #4226, .F. ) ;
#13255=CARTESIAN_POINT ( 'NONE',  ( 10.00000000000000000, 306.0487089519837696, -155.0000000000038369 ) ) ;
#13270=CIRCLE ( 'NONE', #17197, 3.300000000000025135 ) ;
#13281=FILL_AREA_STYLE ('',( #8442 ) ) ;
#13290=LINE ( 'NONE', #789, #9569 ) ;
#13301=DIRECTION ( 'NONE',  ( -1.000000000000000000, -0.000000000000000000, -0.000000000000000000 ) ) ;
#13324=AXIS2_PLACEMENT_3D ( 'NONE', #3855, #7053, #5588 ) ;
#13371=DIRECTION ( 'NONE',  ( -1.000000000000000000, -0.000000000000000000, -0.000000000000000000 ) ) ;
#13375=CARTESIAN_POINT ( 'NONE',  ( 10.00000000000000000, 0.000000000000000000, 0.000000000000000000 ) ) ;
#13377=EDGE_LOOP ( 'NONE', ( #16740, #872, #17016, #10121 ) ) ;
#13378=ORIENTED_EDGE ( 'NONE', *, *, #7247, .F. ) ;
#13380=ORIENTED_EDGE ( 'NONE', *, *, #18466, .T. ) ;
#13396=COLOUR_RGB ( '', 0.09019608, 0.27058824, 0.51372549) ;
#13397=SURFACE_SIDE_STYLE ('',( #12127 ) ) ;
#13445=FILL_AREA_STYLE_COLOUR ( '', #18218 ) ;
#13461=ORIENTED_EDGE ( 'NONE', *, *, #568, .F. ) ;
#13462=PRESENTATION_STYLE_ASSIGNMENT (( #14889 ) ) ;
#13486=( LENGTH_UNIT ( ) NAMED_UNIT ( * ) SI_UNIT ( .MILLI., .METRE. ) );
#13496=SURFACE_SIDE_STYLE ('',( #16402 ) ) ;
#13504=COLOUR_RGB ( '', 0.09019608, 0.27058824, 0.51372549) ;
#13532=AXIS2_PLACEMENT_3D ( 'NONE', #15943, #4412, #8099 ) ;
#13551=PLANE ( 'NONE',  #10207 ) ;
#13555=ORIENTED_EDGE ( 'NONE', *, *, #4117, .T. ) ;
#13558=ORIENTED_EDGE ( 'NONE', *, *, #3595, .T. ) ;
#13567=FILL_AREA_STYLE ('',( #8614 ) ) ;
#13674=( LENGTH_UNIT ( ) NAMED_UNIT ( * ) SI_UNIT ( .MILLI., .METRE. ) );
#13678=( NAMED_UNIT ( * ) SI_UNIT ( $, .STERADIAN. ) SOLID_ANGLE_UNIT ( ) );
#13679=SURFACE_SIDE_STYLE ('',( #9029 ) ) ;
#13699=CIRCLE ( 'NONE', #7456, 3.300000000000025135 ) ;
#13714=CIRCLE ( 'NONE', #16685, 3.300000000000011369 ) ;
#13732=CARTESIAN_POINT ( 'NONE',  ( 0.000000000000000000, 309.2289037985885898, -86.48019484660916589 ) ) ;
#13735=VERTEX_POINT ( 'NONE', #15963 ) ;
#13749=FACE_BOUND ( 'NONE', #762, .T. ) ;
#13771=SURFACE_STYLE_USAGE ( .BOTH. , #13397 ) ;
#13772=CARTESIAN_POINT ( 'NONE',  ( 0.000000000000000000, 301.0487089519826327, 2.148629195649657075E-12 ) ) ;
#13796=SURFACE_STYLE_USAGE ( .BOTH. , #5881 ) ;
#13807=EDGE_LOOP ( 'NONE', ( #11690, #13555 ) ) ;
#13809=DIRECTION ( 'NONE',  ( -1.000000000000000000, -0.000000000000000000, -0.000000000000000000 ) ) ;
#13810=UNCERTAINTY_MEASURE_WITH_UNIT (LENGTH_MEASURE( 1.000000000000000082E-05 ), #8162, 'distance_accuracy_value', 'NONE');
#13827=SURFACE_STYLE_USAGE ( .BOTH. , #10535 ) ;
#13856=ORIENTED_EDGE ( 'NONE', *, *, #1020, .T. ) ;
#13865=( NAMED_UNIT ( * ) PLANE_ANGLE_UNIT ( ) SI_UNIT ( $, .RADIAN. ) );
#13892=EDGE_CURVE ( 'NONE', #17086, #16276, #917, .T. ) ;
#13897=FILL_AREA_STYLE ('',( #19969 ) ) ;
#13941=VERTEX_POINT ( 'NONE', #14973 ) ;
#13972=CARTESIAN_POINT ( 'NONE',  ( 0.000000000000000000, 5.352861011586007481E-13, -75.00000000000599698 ) ) ;
#13981=DIRECTION ( 'NONE',  ( -1.000000000000000000, -0.000000000000000000, -0.000000000000000000 ) ) ;
#13984=DIRECTION ( 'NONE',  ( 0.000000000000000000, 0.000000000000000000, -1.000000000000000000 ) ) ;
#13997=STYLED_ITEM ( 'NONE', ( #11680 ), #13061 ) ;
#14011=( NAMED_UNIT ( * ) PLANE_ANGLE_UNIT ( ) SI_UNIT ( $, .RADIAN. ) );
#14035=FILL_AREA_STYLE ('',( #7942 ) ) ;
#14036=STYLED_ITEM ( 'NONE', ( #2555 ), #2949 ) ;
#14075=CARTESIAN_POINT ( 'NONE',  ( 0.000000000000000000, 341.0487089519837696, -133.5000000000032969 ) ) ;
#14085=CARTESIAN_POINT ( 'NONE',  ( 0.000000000000000000, 341.0487089519837696, -115.0000000000032969 ) ) ;
#14093=VERTEX_POINT ( 'NONE', #15701 ) ;
#14150=ORIENTED_EDGE ( 'NONE', *, *, #574, .T. ) ;
#14174=ORIENTED_EDGE ( 'NONE', *, *, #16245, .F. ) ;
#14176=CARTESIAN_POINT ( 'NONE',  ( 0.000000000000000000, 309.2289037985890445, -146.8198051533984199 ) ) ;
#14177=DIRECTION ( 'NONE',  ( 0.000000000000000000, 0.000000000000000000, -1.000000000000000000 ) ) ;
#14185=( GEOMETRIC_REPRESENTATION_CONTEXT ( 3 ) GLOBAL_UNCERTAINTY_ASSIGNED_CONTEXT ( ( #16748 ) ) GLOBAL_UNIT_ASSIGNED_CONTEXT ( ( #15242, #1185, #18899 ) ) REPRESENTATION_CONTEXT ( 'NONE', 'WORKASPACE' ) );
#14208=ORIENTED_EDGE ( 'NONE', *, *, #5076, .F. ) ;
#14225=SURFACE_STYLE_USAGE ( .BOTH. , #17412 ) ;
#14250=SURFACE_STYLE_USAGE ( .BOTH. , #3015 ) ;
#14287=( GEOMETRIC_REPRESENTATION_CONTEXT ( 3 ) GLOBAL_UNCERTAINTY_ASSIGNED_CONTEXT ( ( #7446 ) ) GLOBAL_UNIT_ASSIGNED_CONTEXT ( ( #19994, #8984, #7462 ) ) REPRESENTATION_CONTEXT ( 'NONE', 'WORKASPACE' ) );
#14291=ORIENTED_EDGE ( 'NONE', *, *, #12574, .T. ) ;
#14320=STYLED_ITEM ( 'NONE', ( #17656 ), #12909 ) ;
#14326=( NAMED_UNIT ( * ) SI_UNIT ( $, .STERADIAN. ) SOLID_ANGLE_UNIT ( ) );
#14338=DIRECTION ( 'NONE',  ( 1.000000000000000000, 0.000000000000000000, 0.000000000000000000 ) ) ;
#14355=VECTOR ( 'NONE', #12796, 1000.000000000000000 ) ;
#14360=( NAMED_UNIT ( * ) PLANE_ANGLE_UNIT ( ) SI_UNIT ( $, .RADIAN. ) );
#14377=CARTESIAN_POINT ( 'NONE',  ( 10.00000000000000000, 309.2289037985890445, -146.8198051533984199 ) ) ;
#14378=FILL_AREA_STYLE_COLOUR ( '', #7922 ) ;
#14386=FACE_OUTER_BOUND ( 'NONE', #16336, .T. ) ;
#14387=CARTESIAN_POINT ( 'NONE',  ( 0.000000000000000000, 376.0487089519832011, -80.00000000000332534 ) ) ;
#14438=VECTOR ( 'NONE', #12825, 1000.000000000000000 ) ;
#14507=AXIS2_PLACEMENT_3D ( 'NONE', #9523, #251, #6552 ) ;
#14563=COLOUR_RGB ( '', 0.31764706, 0.68627451, 0.89019608) ;
#14582=ORIENTED_EDGE ( 'NONE', *, *, #2246, .F. ) ;
#14586=DIRECTION ( 'NONE',  ( -1.000000000000000000, -0.000000000000000000, -0.000000000000000000 ) ) ;
#14588=CLOSED_SHELL ( 'NONE', ( #16376, #4004, #9578, #17573, #7238, #19301, #18459, #10883, #18322, #2545, #13061, #16080, #16712, #4924, #2949, #12371, #15608, #3313, #16744, #930, #1709, #12909, #10139, #12671, #15379, #15054 ) ) ;
#14626=STYLED_ITEM ( 'NONE', ( #12523 ), #10139 ) ;
#14661=ORIENTED_EDGE ( 'NONE', *, *, #431, .T. ) ;
#14672=ORIENTED_EDGE ( 'NONE', *, *, #10982, .F. ) ;
#14686=UNCERTAINTY_MEASURE_WITH_UNIT (LENGTH_MEASURE( 1.000000000000000082E-05 ), #10498, 'distance_accuracy_value', 'NONE');
#14695=DIRECTION ( 'NONE',  ( 1.000000000000000000, -0.000000000000000000, 0.000000000000000000 ) ) ;
#14718=( LENGTH_UNIT ( ) NAMED_UNIT ( * ) SI_UNIT ( .MILLI., .METRE. ) );
#14760=CIRCLE ( 'NONE', #7530, 5.000000000000004441 ) ;
#14781=DIRECTION ( 'NONE',  ( 1.000000000000000000, 0.000000000000000000, -0.000000000000000000 ) ) ;
#14785=SURFACE_STYLE_USAGE ( .BOTH. , #17779 ) ;
#14794=EDGE_CURVE ( 'NONE', #4680, #10259, #3848, .T. ) ;
#14799=EDGE_LOOP ( 'NONE', ( #8507, #5480, #11993, #10285 ) ) ;
#14855=UNCERTAINTY_MEASURE_WITH_UNIT (LENGTH_MEASURE( 1.000000000000000082E-05 ), #14718, 'distance_accuracy_value', 'NONE');
#14864=CARTESIAN_POINT ( 'NONE',  ( 10.00000000000000000, 5.352861011586007481E-13, -75.00000000000599698 ) ) ;
#14868=SURFACE_STYLE_FILL_AREA ( #18047 ) ;
#14884=CARTESIAN_POINT ( 'NONE',  ( 10.00000000000000000, 309.2289037985885898, -79.88019484660914316 ) ) ;
#14889=SURFACE_STYLE_USAGE ( .BOTH. , #18068 ) ;
#14906=VECTOR ( 'NONE', #5892, 1000.000000000000000 ) ;
#14973=CARTESIAN_POINT ( 'NONE',  ( 10.00000000000000000, 372.8685141053778693, -79.88019484660868841 ) ) ;
#14984=SURFACE_STYLE_USAGE ( .BOTH. , #3944 ) ;
#14985=AXIS2_PLACEMENT_3D ( 'NONE', #19766, #8664, #7325 ) ;
#15000=UNCERTAINTY_MEASURE_WITH_UNIT (LENGTH_MEASURE( 1.000000000000000082E-05 ), #16980, 'distance_accuracy_value', 'NONE');
#15003=PLANE ( 'NONE',  #5429 ) ;
#15023=( NAMED_UNIT ( * ) PLANE_ANGLE_UNIT ( ) SI_UNIT ( $, .RADIAN. ) );
#15032=CYLINDRICAL_SURFACE ( 'NONE', #6268, 18.49999999999998934 ) ;
#15035=ORIENTED_EDGE ( 'NONE', *, *, #7247, .T. ) ;
#15043=DIRECTION ( 'NONE',  ( 1.000000000000000000, -0.000000000000000000, -0.000000000000000000 ) ) ;
#15054=ADVANCED_FACE ( 'NONE', ( #15791 ), #7749, .F. ) ;
#15075=DIRECTION ( 'NONE',  ( 0.000000000000000000, 1.000000000000000000, 7.137148015447440312E-15 ) ) ;
#15078=VECTOR ( 'NONE', #1551, 1000.000000000000000 ) ;
#15092=CIRCLE ( 'NONE', #11470, 3.300000000000025135 ) ;
#15117=AXIS2_PLACEMENT_3D ( 'NONE', #11246, #11563, #13130 ) ;
#15127=SURFACE_STYLE_FILL_AREA ( #8749 ) ;
#15162=SURFACE_STYLE_FILL_AREA ( #18038 ) ;
#15170=FILL_AREA_STYLE_COLOUR ( '', #20240 ) ;
#15212=DIRECTION ( 'NONE',  ( -1.000000000000000000, -0.000000000000000000, -0.000000000000000000 ) ) ;
#15242=( LENGTH_UNIT ( ) NAMED_UNIT ( * ) SI_UNIT ( .MILLI., .METRE. ) );
#15250=SURFACE_STYLE_FILL_AREA ( #5875 ) ;
#15301=EDGE_CURVE ( 'NONE', #12228, #7675, #5158, .T. ) ;
#15313=AXIS2_PLACEMENT_3D ( 'NONE', #19078, #332, #12930 ) ;
#15331=( NAMED_UNIT ( * ) SI_UNIT ( $, .STERADIAN. ) SOLID_ANGLE_UNIT ( ) );
#15366=CIRCLE ( 'NONE', #20286, 3.300000000000011369 ) ;
#15369=FILL_AREA_STYLE_COLOUR ( '', #2768 ) ;
#15377=FILL_AREA_STYLE_COLOUR ( '', #841 ) ;
#15379=ADVANCED_FACE ( 'NONE', ( #7400 ), #12046, .F. ) ;
#15393=CARTESIAN_POINT ( 'NONE',  ( 0.000000000000000000, 376.0487089519837127, -155.0000000000033253 ) ) ;
#15419=ORIENTED_EDGE ( 'NONE', *, *, #10008, .F. ) ;
#15438=CARTESIAN_POINT ( 'NONE',  ( 0.000000000000000000, 381.0487089519832011, -80.00000000000332534 ) ) ;
#15460=SURFACE_STYLE_FILL_AREA ( #18826 ) ;
#15479=UNCERTAINTY_MEASURE_WITH_UNIT (LENGTH_MEASURE( 1.000000000000000082E-05 ), #11285, 'distance_accuracy_value', 'NONE');
#15494=CIRCLE ( 'NONE', #17118, 3.300000000000025135 ) ;
#15573=ORIENTED_EDGE ( 'NONE', *, *, #9768, .F. ) ;
#15579=CARTESIAN_POINT ( 'NONE',  ( 10.00000000000000000, 309.2289037985885898, -79.88019484660914316 ) ) ;
#15582=ORIENTED_EDGE ( 'NONE', *, *, #1901, .T. ) ;
#15608=ADVANCED_FACE ( 'NONE', ( #9641 ), #17960, .F. ) ;
#15693=ORIENTED_EDGE ( 'NONE', *, *, #12010, .F. ) ;
#15701=CARTESIAN_POINT ( 'NONE',  ( -75.00000000000000000, 313.8311070602663904, -87.78239810828596035 ) ) ;
#15719=EDGE_LOOP ( 'NONE', ( #5763, #15861, #11080, #19424 ) ) ;
#15724=CARTESIAN_POINT ( 'NONE',  ( 10.00000000000000000, 306.0487089519832011, -75.00000000000380851 ) ) ;
#15787=ORIENTED_EDGE ( 'NONE', *, *, #288, .T. ) ;
#15791=FACE_OUTER_BOUND ( 'NONE', #8613, .T. ) ;
#15816=LINE ( 'NONE', #3442, #14438 ) ;
#15855=DIRECTION ( 'NONE',  ( 1.000000000000000000, -0.000000000000000000, -0.000000000000000000 ) ) ;
#15861=ORIENTED_EDGE ( 'NONE', *, *, #9162, .T. ) ;
#15872=DIRECTION ( 'NONE',  ( 1.000000000000000000, -0.000000000000000000, 0.000000000000000000 ) ) ;
#15875=DIRECTION ( 'NONE',  ( -0.000000000000000000, 1.000000000000000000, 7.137148015447440312E-15 ) ) ;
#15882=FILL_AREA_STYLE ('',( #15369 ) ) ;
#15884=EDGE_LOOP ( 'NONE', ( #19008, #7831, #14582, #13380 ) ) ;
#15926=VECTOR ( 'NONE', #4394, 1000.000000000000000 ) ;
#15931=DIRECTION ( 'NONE',  ( 0.000000000000000000, 0.000000000000000000, -1.000000000000000000 ) ) ;
#15941=SURFACE_STYLE_USAGE ( .BOTH. , #12743 ) ;
#15943=CARTESIAN_POINT ( 'NONE',  ( 10.00000000000000000, 372.8685141053783241, -146.8198051533979935 ) ) ;
#15950=DIRECTION ( 'NONE',  ( 0.000000000000000000, 1.000000000000000000, 0.000000000000000000 ) ) ;
#15963=CARTESIAN_POINT ( 'NONE',  ( 0.000000000000000000, 381.0487089519837127, -150.0000000000032685 ) ) ;
#15975=STYLED_ITEM ( 'NONE', ( #8035 ), #1709 ) ;
#16023=STYLED_ITEM ( 'NONE', ( #4445 ), #2545 ) ;
#16026=EDGE_CURVE ( 'NONE', #4192, #10668, #18577, .T. ) ;
#16055=FILL_AREA_STYLE_COLOUR ( '', #19526 ) ;
#16080=ADVANCED_FACE ( 'NONE', ( #19869 ), #2870, .T. ) ;
#16084=VERTEX_POINT ( 'NONE', #3189 ) ;
#16115=EDGE_CURVE ( 'NONE', #12099, #1949, #286, .T. ) ;
#16122=UNCERTAINTY_MEASURE_WITH_UNIT (LENGTH_MEASURE( 1.000000000000000082E-05 ), #5616, 'distance_accuracy_value', 'NONE');
#16126=UNCERTAINTY_MEASURE_WITH_UNIT (LENGTH_MEASURE( 1.000000000000000082E-05 ), #20166, 'distance_accuracy_value', 'NONE');
#16141=CARTESIAN_POINT ( 'NONE',  ( 10.00000000000000000, 306.0487089519837696, -155.0000000000038369 ) ) ;
#16150=ORIENTED_EDGE ( 'NONE', *, *, #18011, .T. ) ;
#16166=CARTESIAN_POINT ( 'NONE',  ( 10.00000000000000000, 372.8685141053778693, -83.18019484660869978 ) ) ;
#16172=ORIENTED_EDGE ( 'NONE', *, *, #13213, .F. ) ;
#16241=DIRECTION ( 'NONE',  ( 1.000000000000000000, -0.000000000000000000, 0.000000000000000000 ) ) ;
#16245=EDGE_CURVE ( 'NONE', #4860, #10045, #9879, .T. ) ;
#16249=VECTOR ( 'NONE', #4548, 1000.000000000000000 ) ;
#16276=VERTEX_POINT ( 'NONE', #15438 ) ;
#16298=ORIENTED_EDGE ( 'NONE', *, *, #4688, .F. ) ;
#16336=EDGE_LOOP ( 'NONE', ( #9647, #3056, #16172, #6670 ) ) ;
#16356=EDGE_LOOP ( 'NONE', ( #3318, #14174, #14208, #12013 ) ) ;
#16371=( GEOMETRIC_REPRESENTATION_CONTEXT ( 3 ) GLOBAL_UNCERTAINTY_ASSIGNED_CONTEXT ( ( #16126 ) ) GLOBAL_UNIT_ASSIGNED_CONTEXT ( ( #20166, #7718, #1707 ) ) REPRESENTATION_CONTEXT ( 'NONE', 'WORKASPACE' ) );
#16375=AXIS2_PLACEMENT_3D ( 'NONE', #11536, #13301, #11849 ) ;
#16376=ADVANCED_FACE ( 'NONE', ( #5546 ), #15032, .F. ) ;
#16400=EDGE_LOOP ( 'NONE', ( #12020, #13378, #14661, #18730 ) ) ;
#16402=SURFACE_STYLE_FILL_AREA ( #695 ) ;
#16447=UNCERTAINTY_MEASURE_WITH_UNIT (LENGTH_MEASURE( 1.000000000000000082E-05 ), #8201, 'distance_accuracy_value', 'NONE');
#16459=MECHANICAL_DESIGN_GEOMETRIC_PRESENTATION_REPRESENTATION('',(#311),#1596);
#16471=FACE_OUTER_BOUND ( 'NONE', #16400, .T. ) ;
#16477=DIRECTION ( 'NONE',  ( 1.000000000000000000, -0.000000000000000000, 0.000000000000000000 ) ) ;
#16482=MECHANICAL_DESIGN_GEOMETRIC_PRESENTATION_REPRESENTATION('',(#18422),#19083);
#16559=ORIENTED_EDGE ( 'NONE', *, *, #7729, .F. ) ;
#16564=EDGE_LOOP ( 'NONE', ( #7282, #14672, #10652, #11600 ) ) ;
#16567=CARTESIAN_POINT ( 'NONE',  ( 10.00000000000000000, 309.2289037985890445, -143.5198051533984085 ) ) ;
#16595=APPLICATION_CONTEXT ( 'automotive_design' ) ;
#16616=AXIS2_PLACEMENT_3D ( 'NONE', #4411, #18216, #6070 ) ;
#16629=COLOUR_RGB ( '', 0.09019608, 0.27058824, 0.51372549) ;
#16681=LINE ( 'NONE', #8919, #20230 ) ;
#16685=AXIS2_PLACEMENT_3D ( 'NONE', #606, #514, #8355 ) ;
#16691=( NAMED_UNIT ( * ) SI_UNIT ( $, .STERADIAN. ) SOLID_ANGLE_UNIT ( ) );
#16712=ADVANCED_FACE ( 'NONE', ( #12562 ), #18938, .F. ) ;
#16718=( NAMED_UNIT ( * ) SI_UNIT ( $, .STERADIAN. ) SOLID_ANGLE_UNIT ( ) );
#16740=ORIENTED_EDGE ( 'NONE', *, *, #4145, .T. ) ;
#16744=ADVANCED_FACE ( 'NONE', ( #7076, #13749, #7181, #10557, #12106, #7274 ), #13551, .T. ) ;
#16746=AXIS2_PLACEMENT_3D ( 'NONE', #1284, #10600, #2963 ) ;
#16748=UNCERTAINTY_MEASURE_WITH_UNIT (LENGTH_MEASURE( 1.000000000000000082E-05 ), #15242, 'distance_accuracy_value', 'NONE');
#16758=CARTESIAN_POINT ( 'NONE',  ( -75.00000000000000000, 313.8311070602663904, -142.2176018917206761 ) ) ;
#16784=ORIENTED_EDGE ( 'NONE', *, *, #14794, .F. ) ;
#16851=SURFACE_STYLE_FILL_AREA ( #4074 ) ;
#16858=AXIS2_PLACEMENT_3D ( 'NONE', #10994, #6570, #1690 ) ;
#16868=( NAMED_UNIT ( * ) PLANE_ANGLE_UNIT ( ) SI_UNIT ( $, .RADIAN. ) );
#16877=LINE ( 'NONE', #2742, #1219 ) ;
#16893=ORIENTED_EDGE ( 'NONE', *, *, #18890, .F. ) ;
#16897=SURFACE_STYLE_FILL_AREA ( #8940 ) ;
#16944=( GEOMETRIC_REPRESENTATION_CONTEXT ( 3 ) GLOBAL_UNCERTAINTY_ASSIGNED_CONTEXT ( ( #11561 ) ) GLOBAL_UNIT_ASSIGNED_CONTEXT ( ( #6209, #1531, #11134 ) ) REPRESENTATION_CONTEXT ( 'NONE', 'WORKASPACE' ) );
#16952=CARTESIAN_POINT ( 'NONE',  ( -75.00000000000000000, 313.8311070602663904, -142.2176018917206761 ) ) ;
#16978=DIRECTION ( 'NONE',  ( 0.000000000000000000, 0.000000000000000000, 1.000000000000000000 ) ) ;
#16980=( LENGTH_UNIT ( ) NAMED_UNIT ( * ) SI_UNIT ( .MILLI., .METRE. ) );
#17008=FACE_OUTER_BOUND ( 'NONE', #9592, .T. ) ;
#17016=ORIENTED_EDGE ( 'NONE', *, *, #7006, .F. ) ;
#17020=ORIENTED_EDGE ( 'NONE', *, *, #4348, .F. ) ;
#17025=( LENGTH_UNIT ( ) NAMED_UNIT ( * ) SI_UNIT ( .MILLI., .METRE. ) );
#17034=MECHANICAL_DESIGN_GEOMETRIC_PRESENTATION_REPRESENTATION('',(#5517),#9799);
#17086=VERTEX_POINT ( 'NONE', #19760 ) ;
#17089=( NAMED_UNIT ( * ) PLANE_ANGLE_UNIT ( ) SI_UNIT ( $, .RADIAN. ) );
#17093=VECTOR ( 'NONE', #5946, 1000.000000000000000 ) ;
#17118=AXIS2_PLACEMENT_3D ( 'NONE', #892, #8539, #7016 ) ;
#17149=AXIS2_PLACEMENT_3D ( 'NONE', #6501, #1421, #11225 ) ;
#17163=( GEOMETRIC_REPRESENTATION_CONTEXT ( 3 ) GLOBAL_UNCERTAINTY_ASSIGNED_CONTEXT ( ( #7632 ) ) GLOBAL_UNIT_ASSIGNED_CONTEXT ( ( #9447, #265, #3046 ) ) REPRESENTATION_CONTEXT ( 'NONE', 'WORKASPACE' ) );
#17197=AXIS2_PLACEMENT_3D ( 'NONE', #4699, #6260, #13984 ) ;
#17199=EDGE_CURVE ( 'NONE', #11163, #13735, #3076, .T. ) ;
#17212=AXIS2_PLACEMENT_3D ( 'NONE', #14387, #8210, #14177 ) ;
#17216=SURFACE_STYLE_FILL_AREA ( #14035 ) ;
#17244=MECHANICAL_DESIGN_GEOMETRIC_PRESENTATION_REPRESENTATION('',(#11990),#10999);
#17245=FILL_AREA_STYLE ('',( #12505 ) ) ;
#17257=MECHANICAL_DESIGN_GEOMETRIC_PRESENTATION_REPRESENTATION('',(#4101),#6090);
#17267=CARTESIAN_POINT ( 'NONE',  ( 0.000000000000000000, 341.0487089519837696, -115.0000000000032969 ) ) ;
#17271=CARTESIAN_POINT ( 'NONE',  ( -75.00000000000000000, 313.8311070602663904, -87.78239810828596035 ) ) ;
#17299=DIRECTION ( 'NONE',  ( 0.000000000000000000, 1.000000000000000000, 0.000000000000000000 ) ) ;
#17311=FACE_OUTER_BOUND ( 'NONE', #11229, .T. ) ;
#17314=ORIENTED_EDGE ( 'NONE', *, *, #18890, .T. ) ;
#17389=DIRECTION ( 'NONE',  ( 0.000000000000000000, 0.000000000000000000, 1.000000000000000000 ) ) ;
#17391=COLOUR_RGB ( '', 0.66274510, 0.83137255, 0.94901961) ;
#17402=( LENGTH_UNIT ( ) NAMED_UNIT ( * ) SI_UNIT ( .MILLI., .METRE. ) );
#17412=SURFACE_SIDE_STYLE ('',( #17216 ) ) ;
#17417=EDGE_CURVE ( 'NONE', #2260, #5553, #13290, .T. ) ;
#17423=CIRCLE ( 'NONE', #5609, 18.49999999999998934 ) ;
#17464=CARTESIAN_POINT ( 'NONE',  ( 10.00000000000000000, 372.8685141053783241, -150.1198051533980049 ) ) ;
#17536=LINE ( 'NONE', #20323, #576 ) ;
#17539=( NAMED_UNIT ( * ) SI_UNIT ( $, .STERADIAN. ) SOLID_ANGLE_UNIT ( ) );
#17573=ADVANCED_FACE ( 'NONE', ( #9234 ), #11095, .F. ) ;
#17577=( LENGTH_UNIT ( ) NAMED_UNIT ( * ) SI_UNIT ( .MILLI., .METRE. ) );
#17581=EDGE_LOOP ( 'NONE', ( #9014, #18487, #18009, #5193 ) ) ;
#17587=VECTOR ( 'NONE', #7626, 1000.000000000000000 ) ;
#17618=ORIENTED_EDGE ( 'NONE', *, *, #19234, .F. ) ;
#17619=UNCERTAINTY_MEASURE_WITH_UNIT (LENGTH_MEASURE( 1.000000000000000082E-05 ), #3816, 'distance_accuracy_value', 'NONE');
#17656=PRESENTATION_STYLE_ASSIGNMENT (( #6757 ) ) ;
#17671=EDGE_LOOP ( 'NONE', ( #15693, #16559 ) ) ;
#17679=EDGE_CURVE ( 'NONE', #6521, #4192, #11291, .T. ) ;
#17682=DIRECTION ( 'NONE',  ( 0.000000000000000000, 1.000000000000000000, 7.137148015447440312E-15 ) ) ;
#17731=CARTESIAN_POINT ( 'NONE',  ( -75.00000000000000000, 313.8311070602663904, -142.2176018917206761 ) ) ;
#17736=UNCERTAINTY_MEASURE_WITH_UNIT (LENGTH_MEASURE( 1.000000000000000082E-05 ), #637, 'distance_accuracy_value', 'NONE');
#17745=CARTESIAN_POINT ( 'NONE',  ( 10.00000000000000000, 372.8685141053778693, -86.48019484660871115 ) ) ;
#17759=( GEOMETRIC_REPRESENTATION_CONTEXT ( 3 ) GLOBAL_UNCERTAINTY_ASSIGNED_CONTEXT ( ( #8665 ) ) GLOBAL_UNIT_ASSIGNED_CONTEXT ( ( #5784, #9074, #16718 ) ) REPRESENTATION_CONTEXT ( 'NONE', 'WORKASPACE' ) );
#17772=VECTOR ( 'NONE', #3686, 1000.000000000000000 ) ;
#17779=SURFACE_SIDE_STYLE ('',( #261 ) ) ;
#17790=ORIENTED_EDGE ( 'NONE', *, *, #4348, .T. ) ;
#17863=DIRECTION ( 'NONE',  ( 1.000000000000000000, -0.000000000000000000, 0.000000000000000000 ) ) ;
#17884=ORIENTED_EDGE ( 'NONE', *, *, #5476, .T. ) ;
#17892=DIRECTION ( 'NONE',  ( -1.000000000000000000, -0.000000000000000000, -0.000000000000000000 ) ) ;
#17899=DIRECTION ( 'NONE',  ( 1.000000000000000000, -0.000000000000000000, 0.000000000000000000 ) ) ;
#17942=VERTEX_POINT ( 'NONE', #16141 ) ;
#17960=CYLINDRICAL_SURFACE ( 'NONE', #13324, 3.300000000000025135 ) ;
#17961=CARTESIAN_POINT ( 'NONE',  ( 10.00000000000000000, 341.0487089519837696, -115.0000000000032969 ) ) ;
#17962=AXIS2_PLACEMENT_3D ( 'NONE', #11479, #17863, #18340 ) ;
#17982=( NAMED_UNIT ( * ) SI_UNIT ( $, .STERADIAN. ) SOLID_ANGLE_UNIT ( ) );
#18009=ORIENTED_EDGE ( 'NONE', *, *, #19508, .F. ) ;
#18011=EDGE_CURVE ( 'NONE', #5553, #9832, #18813, .T. ) ;
#18038=FILL_AREA_STYLE ('',( #10123 ) ) ;
#18047=FILL_AREA_STYLE ('',( #19391 ) ) ;
#18051=EDGE_LOOP ( 'NONE', ( #14291, #3656, #19171, #10159 ) ) ;
#18067=LINE ( 'NONE', #11712, #1899 ) ;
#18068=SURFACE_SIDE_STYLE ('',( #16851 ) ) ;
#18134=( NAMED_UNIT ( * ) PLANE_ANGLE_UNIT ( ) SI_UNIT ( $, .RADIAN. ) );
#18141=( NAMED_UNIT ( * ) SI_UNIT ( $, .STERADIAN. ) SOLID_ANGLE_UNIT ( ) );
#18165=( NAMED_UNIT ( * ) PLANE_ANGLE_UNIT ( ) SI_UNIT ( $, .RADIAN. ) );
#18198=FACE_OUTER_BOUND ( 'NONE', #18315, .T. ) ;
#18199=CARTESIAN_POINT ( 'NONE',  ( -75.00000000000000000, 313.8311070602663904, -142.2176018917206761 ) ) ;
#18201=EDGE_CURVE ( 'NONE', #4515, #4998, #20349, .T. ) ;
#18214=EDGE_CURVE ( 'NONE', #4998, #2140, #13270, .T. ) ;
#18216=DIRECTION ( 'NONE',  ( 1.000000000000000000, -0.000000000000000000, 0.000000000000000000 ) ) ;
#18218=COLOUR_RGB ( '', 0.08235294, 0.09019608, 0.10196078) ;
#18228=CIRCLE ( 'NONE', #4759, 3.300000000000025135 ) ;
#18248=( NAMED_UNIT ( * ) SI_UNIT ( $, .STERADIAN. ) SOLID_ANGLE_UNIT ( ) );
#18301=PRESENTATION_STYLE_ASSIGNMENT (( #5935 ) ) ;
#18307=( NAMED_UNIT ( * ) PLANE_ANGLE_UNIT ( ) SI_UNIT ( $, .RADIAN. ) );
#18311=( NAMED_UNIT ( * ) SI_UNIT ( $, .STERADIAN. ) SOLID_ANGLE_UNIT ( ) );
#18315=EDGE_LOOP ( 'NONE', ( #9298, #7622, #16298, #17314 ) ) ;
#18322=ADVANCED_FACE ( 'NONE', ( #14386 ), #6111, .F. ) ;
#18336=CARTESIAN_POINT ( 'NONE',  ( 10.00000000000000000, 306.0487089519837127, -150.0000000000038369 ) ) ;
#18340=DIRECTION ( 'NONE',  ( 0.000000000000000000, 0.000000000000000000, -1.000000000000000000 ) ) ;
#18362=ORIENTED_EDGE ( 'NONE', *, *, #15301, .T. ) ;
#18386=SURFACE_SIDE_STYLE ('',( #1059 ) ) ;
#18389=AXIS2_PLACEMENT_3D ( 'NONE', #12252, #10504, #7525 ) ;
#18390=SURFACE_STYLE_FILL_AREA ( #9131 ) ;
#18400=FILL_AREA_STYLE_COLOUR ( '', #1783 ) ;
#18404=PRESENTATION_STYLE_ASSIGNMENT (( #4212 ) ) ;
#18422=STYLED_ITEM ( 'NONE', ( #13462 ), #16744 ) ;
#18431=VERTEX_POINT ( 'NONE', #9696 ) ;
#18448=DIRECTION ( 'NONE',  ( 0.000000000000000000, 0.000000000000000000, -1.000000000000000000 ) ) ;
#18454=DIRECTION ( 'NONE',  ( 0.000000000000000000, 0.000000000000000000, -1.000000000000000000 ) ) ;
#18459=ADVANCED_FACE ( 'NONE', ( #18198 ), #4103, .F. ) ;
#18466=EDGE_CURVE ( 'NONE', #4537, #18431, #12125, .T. ) ;
#18487=ORIENTED_EDGE ( 'NONE', *, *, #1655, .F. ) ;
#18488=PRESENTATION_STYLE_ASSIGNMENT (( #10374 ) ) ;
#18515=FACE_OUTER_BOUND ( 'NONE', #18051, .T. ) ;
#18529=DIRECTION ( 'NONE',  ( 1.000000000000000000, 0.000000000000000000, 0.000000000000000000 ) ) ;
#18535=CARTESIAN_POINT ( 'NONE',  ( -75.00000000000000000, 313.8311070602663904, -142.2176018917206761 ) ) ;
#18559=FACE_BOUND ( 'NONE', #997, .T. ) ;
#18568=LINE ( 'NONE', #16567, #60 ) ;
#18577=CIRCLE ( 'NONE', #12339, 18.49999999999998934 ) ;
#18586=ORIENTED_EDGE ( 'NONE', *, *, #4611, .T. ) ;
#18590=PRODUCT_CONTEXT ( 'NONE', #19702, 'mechanical' ) ;
#18651=ORIENTED_EDGE ( 'NONE', *, *, #12010, .T. ) ;
#18654=LINE ( 'NONE', #1112, #9654 ) ;
#18671=EDGE_CURVE ( 'NONE', #16276, #18431, #5697, .T. ) ;
#18730=ORIENTED_EDGE ( 'NONE', *, *, #19124, .T. ) ;
#18763=ORIENTED_EDGE ( 'NONE', *, *, #11280, .F. ) ;
#18779=DIRECTION ( 'NONE',  ( 1.000000000000000000, -0.000000000000000000, 0.000000000000000000 ) ) ;
#18789=( NAMED_UNIT ( * ) PLANE_ANGLE_UNIT ( ) SI_UNIT ( $, .RADIAN. ) );
#18793=DIRECTION ( 'NONE',  ( 0.000000000000000000, 0.000000000000000000, -1.000000000000000000 ) ) ;
#18813=CIRCLE ( 'NONE', #8617, 3.300000000000011369 ) ;
#18820=DIRECTION ( 'NONE',  ( -1.000000000000000000, -0.000000000000000000, -0.000000000000000000 ) ) ;
#18826=FILL_AREA_STYLE ('',( #6485 ) ) ;
#18845=STYLED_ITEM ( 'NONE', ( #3414 ), #18459 ) ;
#18879=FACE_OUTER_BOUND ( 'NONE', #8913, .T. ) ;
#18890=EDGE_CURVE ( 'NONE', #17942, #4680, #7077, .T. ) ;
#18898=DIRECTION ( 'NONE',  ( 0.000000000000000000, -0.000000000000000000, -1.000000000000000000 ) ) ;
#18899=( NAMED_UNIT ( * ) SI_UNIT ( $, .STERADIAN. ) SOLID_ANGLE_UNIT ( ) );
#18908=DIRECTION ( 'NONE',  ( 1.000000000000000000, -0.000000000000000000, -0.000000000000000000 ) ) ;
#18935=DIRECTION ( 'NONE',  ( 0.000000000000000000, 0.000000000000000000, -1.000000000000000000 ) ) ;
#18938=PLANE ( 'NONE',  #4952 ) ;
#18949=EDGE_LOOP ( 'NONE', ( #2201, #19686, #2233, #10933 ) ) ;
#18958=PRODUCT ( 'Part4', 'Part4', '', ( #18590 ) ) ;
#18996=CARTESIAN_POINT ( 'NONE',  ( -75.00000000000000000, 313.8311070602663904, -87.78239810828596035 ) ) ;
#19008=ORIENTED_EDGE ( 'NONE', *, *, #10008, .T. ) ;
#19078=CARTESIAN_POINT ( 'NONE',  ( -75.00000000000000000, 313.8311070602663904, -87.78239810828596035 ) ) ;
#19081=CYLINDRICAL_SURFACE ( 'NONE', #9491, 3.300000000000025135 ) ;
#19083=( GEOMETRIC_REPRESENTATION_CONTEXT ( 3 ) GLOBAL_UNCERTAINTY_ASSIGNED_CONTEXT ( ( #16122 ) ) GLOBAL_UNIT_ASSIGNED_CONTEXT ( ( #5616, #18165, #17982 ) ) REPRESENTATION_CONTEXT ( 'NONE', 'WORKASPACE' ) );
#19086=CIRCLE ( 'NONE', #15117, 5.000000000000004441 ) ;
#19124=EDGE_CURVE ( 'NONE', #10668, #4192, #4085, .T. ) ;
#19133=CYLINDRICAL_SURFACE ( 'NONE', #764, 3.300000000000011369 ) ;
#19135=CARTESIAN_POINT ( 'NONE',  ( 10.00000000000000000, 341.0487089519837696, -96.50000000000331113 ) ) ;
#19146=DIRECTION ( 'NONE',  ( 0.000000000000000000, 0.000000000000000000, -1.000000000000000000 ) ) ;
#19171=ORIENTED_EDGE ( 'NONE', *, *, #574, .F. ) ;
#19230=FILL_AREA_STYLE ('',( #2203 ) ) ;
#19234=EDGE_CURVE ( 'NONE', #6758, #16084, #4168, .T. ) ;
#19264=DIRECTION ( 'NONE',  ( -1.000000000000000000, -0.000000000000000000, -0.000000000000000000 ) ) ;
#19284=AXIS2_PLACEMENT_3D ( 'NONE', #5798, #6204, #12385 ) ;
#19301=ADVANCED_FACE ( 'NONE', ( #4457, #7348, #18559, #19897, #927, #7250 ), #5903, .F. ) ;
#19333=EDGE_LOOP ( 'NONE', ( #13242, #1107 ) ) ;
#19389=VERTEX_POINT ( 'NONE', #11140 ) ;
#19391=FILL_AREA_STYLE_COLOUR ( '', #454 ) ;
#19424=ORIENTED_EDGE ( 'NONE', *, *, #4611, .F. ) ;
#19485=( NAMED_UNIT ( * ) PLANE_ANGLE_UNIT ( ) SI_UNIT ( $, .RADIAN. ) );
#19508=EDGE_CURVE ( 'NONE', #8713, #11104, #6621, .T. ) ;
#19509=EDGE_LOOP ( 'NONE', ( #5736, #8509 ) ) ;
#19526=COLOUR_RGB ( '', 0.09019608, 0.27058824, 0.51372549) ;
#19528=LINE ( 'NONE', #13097, #9707 ) ;
#19538=( GEOMETRIC_REPRESENTATION_CONTEXT ( 3 ) GLOBAL_UNCERTAINTY_ASSIGNED_CONTEXT ( ( #7065 ) ) GLOBAL_UNIT_ASSIGNED_CONTEXT ( ( #17402, #6601, #14326 ) ) REPRESENTATION_CONTEXT ( 'NONE', 'WORKASPACE' ) );
#19561=AXIS2_PLACEMENT_3D ( 'NONE', #7290, #12320, #10469 ) ;
#19567=AXIS2_PLACEMENT_3D ( 'NONE', #14864, #1015, #15075 ) ;
#19614=DIRECTION ( 'NONE',  ( 0.000000000000000000, 0.000000000000000000, -1.000000000000000000 ) ) ;
#19620=ORIENTED_EDGE ( 'NONE', *, *, #6604, .T. ) ;
#19643=SURFACE_STYLE_USAGE ( .BOTH. , #13496 ) ;
#19667=ORIENTED_EDGE ( 'NONE', *, *, #568, .T. ) ;
#19686=ORIENTED_EDGE ( 'NONE', *, *, #17679, .T. ) ;
#19700=DIRECTION ( 'NONE',  ( 0.000000000000000000, -0.000000000000000000, 1.000000000000000000 ) ) ;
#19702=APPLICATION_CONTEXT ( 'automotive_design' ) ;
#19718=DIRECTION ( 'NONE',  ( 1.000000000000000000, -0.000000000000000000, 0.000000000000000000 ) ) ;
#19747=( NAMED_UNIT ( * ) SI_UNIT ( $, .STERADIAN. ) SOLID_ANGLE_UNIT ( ) );
#19760=CARTESIAN_POINT ( 'NONE',  ( 10.00000000000000000, 381.0487089519832011, -80.00000000000332534 ) ) ;
#19766=CARTESIAN_POINT ( 'NONE',  ( 10.00000000000000000, 306.0487089519832011, -80.00000000000380851 ) ) ;
#19792=ORIENTED_EDGE ( 'NONE', *, *, #7846, .T. ) ;
#19798=( GEOMETRIC_REPRESENTATION_CONTEXT ( 3 ) GLOBAL_UNCERTAINTY_ASSIGNED_CONTEXT ( ( #4115 ) ) GLOBAL_UNIT_ASSIGNED_CONTEXT ( ( #17577, #11189, #6262 ) ) REPRESENTATION_CONTEXT ( 'NONE', 'WORKASPACE' ) );
#19840=LINE ( 'NONE', #13772, #12834 ) ;
#19842=( NAMED_UNIT ( * ) PLANE_ANGLE_UNIT ( ) SI_UNIT ( $, .RADIAN. ) );
#19844=AXIS2_PLACEMENT_3D ( 'NONE', #13007, #5262, #8353 ) ;
#19869=FACE_OUTER_BOUND ( 'NONE', #6949, .T. ) ;
#19882=COLOUR_RGB ( '', 0.31764706, 0.68627451, 0.89019608) ;
#19883=SURFACE_STYLE_FILL_AREA ( #1211 ) ;
#19897=FACE_BOUND ( 'NONE', #13807, .T. ) ;
#19913=FILL_AREA_STYLE ('',( #2406 ) ) ;
#19934=FILL_AREA_STYLE_COLOUR ( '', #8320 ) ;
#19956=PRESENTATION_STYLE_ASSIGNMENT (( #2856 ) ) ;
#19969=FILL_AREA_STYLE_COLOUR ( '', #8725 ) ;
#19994=( LENGTH_UNIT ( ) NAMED_UNIT ( * ) SI_UNIT ( .MILLI., .METRE. ) );
#20008=FILL_AREA_STYLE_COLOUR ( '', #6935 ) ;
#20057=FACE_OUTER_BOUND ( 'NONE', #8247, .T. ) ;
#20060=CARTESIAN_POINT ( 'NONE',  ( 0.000000000000000000, 368.2663108437010919, -87.78239810828596035 ) ) ;
#20076=LINE ( 'NONE', #18535, #17587 ) ;
#20088=PRODUCT_DEFINITION_SHAPE ( 'NONE', 'NONE',  #1380 ) ;
#20100=DIRECTION ( 'NONE',  ( -1.000000000000000000, -0.000000000000000000, -0.000000000000000000 ) ) ;
#20166=( LENGTH_UNIT ( ) NAMED_UNIT ( * ) SI_UNIT ( .MILLI., .METRE. ) );
#20194=( NAMED_UNIT ( * ) SI_UNIT ( $, .STERADIAN. ) SOLID_ANGLE_UNIT ( ) );
#20210=AXIS2_PLACEMENT_3D ( 'NONE', #4945, #6495, #19146 ) ;
#20224=STYLED_ITEM ( 'NONE', ( #10604 ), #16080 ) ;
#20230=VECTOR ( 'NONE', #15212, 1000.000000000000000 ) ;
#20240=COLOUR_RGB ( '', 0.72549020, 0.75294118, 0.79215686) ;
#20263=SURFACE_STYLE_USAGE ( .BOTH. , #9539 ) ;
#20286=AXIS2_PLACEMENT_3D ( 'NONE', #3679, #19718, #8731 ) ;
#20323=CARTESIAN_POINT ( 'NONE',  ( 10.00000000000000000, 301.0487089519826327, 2.148629195649657075E-12 ) ) ;
#20325=AXIS2_PLACEMENT_3D ( 'NONE', #3183, #15872, #18935 ) ;
#20342=DIRECTION ( 'NONE',  ( 1.000000000000000000, 0.000000000000000000, 0.000000000000000000 ) ) ;
#20349=LINE ( 'NONE', #17464, #2036 ) ;
ENDSEC;
END-ISO-10303-21;
